ISO-10303-21;
HEADER;
/* Generated by software containing ST-Developer
 * from STEP Tools, Inc. (www.steptools.com) 
 */

FILE_DESCRIPTION(
/* description */ ('Turntable on roller ring'),
/* implementation_level */ '2;1');

FILE_NAME(
/* name */ 'Cage (1).step',
/* time_stamp */ '2026-10-28T03:23:59-07:00',
/* author */ (''),
/* organization */ (''),
/* preprocessor_version */ 'ST-DEVELOPER v20.2',
/* originating_system */ 'Autodesk Translation Framework v15.17.0.0',
/* authorisation */ '');

FILE_SCHEMA (('AUTOMOTIVE_DESIGN { 1 0 10303 214 3 1 1 }'));
ENDSEC;

DATA;
#10=MECHANICAL_DESIGN_GEOMETRIC_PRESENTATION_REPRESENTATION('',(#686),#16281);
#420=B_SPLINE_CURVE_WITH_KNOTS('',3,(#15640,#15641,#15642,#15643,#15644,
#15645,#15646,#15647,#15648,#15649,#15650,#15651,#15652,#15653,#15654,#15655,
#15656,#15657,#15658,#15659,#15660,#15661),.UNSPECIFIED.,.F.,.F.,(4,2,2,
2,2,2,2,2,2,2,4),(0.0473477652366656,0.126350602536658,0.189525903804987,
0.252701205073317,0.313298422430275,0.373895639787233,0.434492857144191,
0.495090074501149,0.558265375769478,0.621440677037807,0.7004435143378),
 .UNSPECIFIED.);
#421=B_SPLINE_CURVE_WITH_KNOTS('',3,(#15665,#15666,#15667,#15668,#15669,
#15670,#15671,#15672,#15673,#15674,#15675,#15676,#15677,#15678,#15679,#15680,
#15681,#15682,#15683,#15684,#15685,#15686),.UNSPECIFIED.,.F.,.F.,(4,2,2,
2,2,2,2,2,2,2,4),(0.0464897534940957,0.0852567806515119,0.170513561303024,
0.246687263103517,0.308657850341199,0.370628437578881,0.432599024816563,
0.494569612054245,0.570743313854739,0.656000094506251,0.694767121663666),
 .UNSPECIFIED.);
#422=B_SPLINE_CURVE_WITH_KNOTS('',3,(#15692,#15693,#15694,#15695,#15696,
#15697,#15698,#15699,#15700,#15701,#15702,#15703,#15704,#15705,#15706,#15707,
#15708,#15709,#15710,#15711,#15712,#15713),.UNSPECIFIED.,.F.,.F.,(4,2,2,
2,2,2,2,2,2,2,4),(0.0464897534940957,0.0852567806515118,0.170513561303024,
0.246687263103517,0.308657850341199,0.370628437578881,0.432599024816563,
0.494569612054245,0.570743313854738,0.65600009450625,0.694767121663666),
 .UNSPECIFIED.);
#423=B_SPLINE_CURVE_WITH_KNOTS('',3,(#15717,#15718,#15719,#15720,#15721,
#15722,#15723,#15724,#15725,#15726,#15727,#15728,#15729,#15730,#15731,#15732,
#15733,#15734,#15735,#15736,#15737,#15738),.UNSPECIFIED.,.F.,.F.,(4,2,2,
2,2,2,2,2,2,2,4),(0.0464897534940957,0.0852567806515119,0.170513561303024,
0.246687263103517,0.308657850341199,0.370628437578881,0.432599024816563,
0.494569612054245,0.570743313854739,0.656000094506251,0.694767121663666),
 .UNSPECIFIED.);
#424=B_SPLINE_CURVE_WITH_KNOTS('',3,(#15742,#15743,#15744,#15745,#15746,
#15747,#15748,#15749,#15750,#15751,#15752,#15753),.UNSPECIFIED.,.F.,.F.,
(4,2,2,2,2,4),(0.0464897534940957,0.0852567806515119,0.170513561303024,
0.246687263103517,0.308657850341199,0.370628437578881),.UNSPECIFIED.);
#425=B_SPLINE_CURVE_WITH_KNOTS('',3,(#15758,#15759,#15760,#15761,#15762,
#15763,#15764,#15765,#15766,#15767,#15768,#15769),.UNSPECIFIED.,.F.,.F.,
(4,2,2,2,2,4),(0.370628437578881,0.432599024816563,0.494569612054245,0.570743313854738,
0.65600009450625,0.694767121663666),.UNSPECIFIED.);
#426=B_SPLINE_CURVE_WITH_KNOTS('',3,(#15773,#15774,#15775,#15776,#15777,
#15778,#15779,#15780,#15781,#15782,#15783,#15784,#15785,#15786,#15787,#15788,
#15789,#15790,#15791,#15792,#15793,#15794),.UNSPECIFIED.,.F.,.F.,(4,2,2,
2,2,2,2,2,2,2,4),(0.0464897534940957,0.0852567806515121,0.170513561303024,
0.246687263103518,0.308657850341199,0.370628437578881,0.432599024816563,
0.494569612054245,0.570743313854738,0.65600009450625,0.694767121663666),
 .UNSPECIFIED.);
#427=B_SPLINE_CURVE_WITH_KNOTS('',3,(#15798,#15799,#15800,#15801,#15802,
#15803,#15804,#15805,#15806,#15807,#15808,#15809,#15810,#15811,#15812,#15813,
#15814,#15815,#15816,#15817,#15818,#15819),.UNSPECIFIED.,.F.,.F.,(4,2,2,
2,2,2,2,2,2,2,4),(0.0464897534940957,0.0852567806515119,0.170513561303024,
0.246687263103517,0.308657850341199,0.370628437578881,0.432599024816563,
0.494569612054245,0.570743313854738,0.65600009450625,0.694767121663667),
 .UNSPECIFIED.);
#428=B_SPLINE_CURVE_WITH_KNOTS('',3,(#15823,#15824,#15825,#15826,#15827,
#15828,#15829,#15830,#15831,#15832,#15833,#15834,#15835,#15836,#15837,#15838,
#15839,#15840,#15841,#15842,#15843,#15844),.UNSPECIFIED.,.F.,.F.,(4,2,2,
2,2,2,2,2,2,2,4),(0.0464897534940957,0.0852567806515119,0.170513561303024,
0.246687263103517,0.308657850341199,0.370628437578881,0.432599024816563,
0.494569612054245,0.570743313854738,0.65600009450625,0.694767121663666),
 .UNSPECIFIED.);
#429=B_SPLINE_CURVE_WITH_KNOTS('',3,(#15848,#15849,#15850,#15851,#15852,
#15853,#15854,#15855,#15856,#15857,#15858,#15859,#15860,#15861,#15862,#15863,
#15864,#15865,#15866,#15867,#15868,#15869),.UNSPECIFIED.,.F.,.F.,(4,2,2,
2,2,2,2,2,2,2,4),(0.0464897534940957,0.0852567806515119,0.170513561303024,
0.246687263103517,0.308657850341199,0.370628437578881,0.432599024816563,
0.494569612054245,0.570743313854739,0.656000094506251,0.694767121663667),
 .UNSPECIFIED.);
#430=B_SPLINE_CURVE_WITH_KNOTS('',3,(#15877,#15878,#15879,#15880,#15881,
#15882,#15883,#15884,#15885,#15886,#15887,#15888,#15889,#15890,#15891,#15892,
#15893,#15894,#15895,#15896,#15897,#15898),.UNSPECIFIED.,.F.,.F.,(4,2,2,
2,2,2,2,2,2,2,4),(0.0473477652366656,0.126350602536658,0.189525903804987,
0.252701205073316,0.313298422430274,0.373895639787232,0.434492857144191,
0.495090074501149,0.558265375769478,0.621440677037807,0.7004435143378),
 .UNSPECIFIED.);
#431=B_SPLINE_CURVE_WITH_KNOTS('',3,(#15906,#15907,#15908,#15909,#15910,
#15911,#15912,#15913,#15914,#15915,#15916,#15917,#15918,#15919,#15920,#15921,
#15922,#15923,#15924,#15925,#15926,#15927),.UNSPECIFIED.,.F.,.F.,(4,2,2,
2,2,2,2,2,2,2,4),(0.0473477652366656,0.126350602536658,0.189525903804987,
0.252701205073317,0.313298422430275,0.373895639787233,0.434492857144191,
0.495090074501149,0.558265375769478,0.621440677037807,0.7004435143378),
 .UNSPECIFIED.);
#432=B_SPLINE_CURVE_WITH_KNOTS('',3,(#15936,#15937,#15938,#15939,#15940,
#15941,#15942,#15943,#15944,#15945,#15946,#15947),.UNSPECIFIED.,.F.,.F.,
(4,2,2,2,2,4),(0.0473477652366656,0.126350602536658,0.189525903804987,0.252701205073316,
0.313298422430275,0.373895639787233),.UNSPECIFIED.);
#433=B_SPLINE_CURVE_WITH_KNOTS('',3,(#15949,#15950,#15951,#15952,#15953,
#15954,#15955,#15956,#15957,#15958,#15959,#15960),.UNSPECIFIED.,.F.,.F.,
(4,2,2,2,2,4),(0.373895639787233,0.434492857144191,0.495090074501149,0.558265375769478,
0.621440677037807,0.7004435143378),.UNSPECIFIED.);
#434=B_SPLINE_CURVE_WITH_KNOTS('',3,(#15967,#15968,#15969,#15970,#15971,
#15972,#15973,#15974,#15975,#15976,#15977,#15978,#15979,#15980,#15981,#15982,
#15983,#15984,#15985,#15986,#15987,#15988),.UNSPECIFIED.,.F.,.F.,(4,2,2,
2,2,2,2,2,2,2,4),(0.0473477652366656,0.126350602536658,0.189525903804987,
0.252701205073316,0.313298422430275,0.373895639787233,0.434492857144191,
0.495090074501149,0.558265375769478,0.621440677037807,0.7004435143378),
 .UNSPECIFIED.);
#435=B_SPLINE_CURVE_WITH_KNOTS('',3,(#15996,#15997,#15998,#15999,#16000,
#16001,#16002,#16003,#16004,#16005,#16006,#16007,#16008,#16009,#16010,#16011,
#16012,#16013,#16014,#16015,#16016,#16017),.UNSPECIFIED.,.F.,.F.,(4,2,2,
2,2,2,2,2,2,2,4),(0.0473477652366656,0.126350602536658,0.189525903804987,
0.252701205073317,0.313298422430275,0.373895639787233,0.434492857144191,
0.495090074501149,0.558265375769478,0.621440677037807,0.7004435143378),
 .UNSPECIFIED.);
#436=B_SPLINE_CURVE_WITH_KNOTS('',3,(#16025,#16026,#16027,#16028,#16029,
#16030,#16031,#16032,#16033,#16034,#16035,#16036,#16037,#16038,#16039,#16040,
#16041,#16042,#16043,#16044,#16045,#16046),.UNSPECIFIED.,.F.,.F.,(4,2,2,
2,2,2,2,2,2,2,4),(0.0473477652366656,0.126350602536658,0.189525903804987,
0.252701205073316,0.313298422430275,0.373895639787233,0.434492857144191,
0.495090074501149,0.558265375769478,0.621440677037807,0.7004435143378),
 .UNSPECIFIED.);
#437=B_SPLINE_CURVE_WITH_KNOTS('',3,(#16055,#16056,#16057,#16058,#16059,
#16060,#16061,#16062,#16063,#16064,#16065,#16066,#16067,#16068,#16069,#16070,
#16071,#16072,#16073,#16074,#16075,#16076),.UNSPECIFIED.,.F.,.F.,(4,2,2,
2,2,2,2,2,2,2,4),(0.0473477652366656,0.126350602536658,0.189525903804987,
0.252701205073317,0.313298422430275,0.373895639787233,0.434492857144191,
0.495090074501149,0.558265375769478,0.621440677037807,0.7004435143378),
 .UNSPECIFIED.);
#464=SPHERICAL_SURFACE('',#10099,0.247676);
#465=SPHERICAL_SURFACE('',#10115,0.247676);
#466=SPHERICAL_SURFACE('',#10120,0.247676);
#467=SPHERICAL_SURFACE('',#10125,0.247676);
#468=SPHERICAL_SURFACE('',#10130,0.247676);
#469=SPHERICAL_SURFACE('',#10135,0.247676);
#470=SPHERICAL_SURFACE('',#10140,0.247676);
#471=SPHERICAL_SURFACE('',#10148,0.247676);
#560=SHAPE_REPRESENTATION_RELATIONSHIP('SRR','None',#16585,#615);
#615=ADVANCED_BREP_SHAPE_REPRESENTATION('',(#754),#16279);
#686=STYLED_ITEM('',(#16932),#754);
#754=MANIFOLD_SOLID_BREP('Continuous crown cage',#8431);
#985=FACE_BOUND('',#2479,.T.);
#1237=PLANE('',#10112);
#1238=PLANE('',#10117);
#1239=PLANE('',#10122);
#1240=PLANE('',#10127);
#1241=PLANE('',#10132);
#1242=PLANE('',#10137);
#1243=PLANE('',#10146);
#1244=PLANE('',#10150);
#1245=PLANE('',#10151);
#1728=FACE_OUTER_BOUND('',#2461,.T.);
#1729=FACE_OUTER_BOUND('',#2462,.T.);
#1730=FACE_OUTER_BOUND('',#2463,.T.);
#1731=FACE_OUTER_BOUND('',#2464,.T.);
#1732=FACE_OUTER_BOUND('',#2465,.T.);
#1733=FACE_OUTER_BOUND('',#2466,.T.);
#1734=FACE_OUTER_BOUND('',#2467,.T.);
#1735=FACE_OUTER_BOUND('',#2468,.T.);
#1736=FACE_OUTER_BOUND('',#2469,.T.);
#1737=FACE_OUTER_BOUND('',#2470,.T.);
#1738=FACE_OUTER_BOUND('',#2471,.T.);
#1739=FACE_OUTER_BOUND('',#2472,.T.);
#1740=FACE_OUTER_BOUND('',#2473,.T.);
#1741=FACE_OUTER_BOUND('',#2474,.T.);
#1742=FACE_OUTER_BOUND('',#2475,.T.);
#1743=FACE_OUTER_BOUND('',#2476,.T.);
#1744=FACE_OUTER_BOUND('',#2477,.T.);
#1745=FACE_OUTER_BOUND('',#2478,.T.);
#1746=FACE_OUTER_BOUND('',#2480,.T.);
#2461=EDGE_LOOP('',(#7537,#7538,#7539,#7540));
#2462=EDGE_LOOP('',(#7541,#7542,#7543,#7544,#7545,#7546,#7547,#7548,#7549,
#7550,#7551,#7552,#7553,#7554,#7555,#7556,#7557,#7558,#7559,#7560));
#2463=EDGE_LOOP('',(#7561,#7562,#7563,#7564));
#2464=EDGE_LOOP('',(#7565,#7566,#7567,#7568));
#2465=EDGE_LOOP('',(#7569,#7570,#7571,#7572));
#2466=EDGE_LOOP('',(#7573,#7574,#7575,#7576));
#2467=EDGE_LOOP('',(#7577,#7578,#7579,#7580));
#2468=EDGE_LOOP('',(#7581,#7582,#7583,#7584,#7585,#7586));
#2469=EDGE_LOOP('',(#7587,#7588,#7589,#7590));
#2470=EDGE_LOOP('',(#7591,#7592,#7593,#7594));
#2471=EDGE_LOOP('',(#7595,#7596,#7597,#7598));
#2472=EDGE_LOOP('',(#7599,#7600,#7601,#7602));
#2473=EDGE_LOOP('',(#7603,#7604,#7605,#7606));
#2474=EDGE_LOOP('',(#7607,#7608,#7609,#7610));
#2475=EDGE_LOOP('',(#7611,#7612,#7613,#7614,#7615,#7616,#7617,#7618,#7619,
#7620,#7621,#7622,#7623,#7624,#7625,#7626,#7627,#7628,#7629,#7630));
#2476=EDGE_LOOP('',(#7631,#7632,#7633,#7634));
#2477=EDGE_LOOP('',(#7635,#7636,#7637,#7638));
#2478=EDGE_LOOP('',(#7639));
#2479=EDGE_LOOP('',(#7640));
#2480=EDGE_LOOP('',(#7641,#7642,#7643,#7644));
#2970=LINE('',#15755,#3453);
#2971=LINE('',#16051,#3454);
#3453=VECTOR('',#12809,1.019052);
#3454=VECTOR('',#12886,0.980948);
#3907=CIRCLE('',#10100,0.243053047864041);
#3908=CIRCLE('',#10101,0.243053047864041);
#3909=CIRCLE('',#10103,1.019052);
#3910=CIRCLE('',#10104,1.019052);
#3911=CIRCLE('',#10105,1.019052);
#3912=CIRCLE('',#10106,1.019052);
#3913=CIRCLE('',#10107,1.019052);
#3914=CIRCLE('',#10108,1.019052);
#3915=CIRCLE('',#10109,1.019052);
#3916=CIRCLE('',#10110,1.019052);
#3917=CIRCLE('',#10111,1.019052);
#3918=CIRCLE('',#10113,0.980948);
#3919=CIRCLE('',#10114,0.243053047864041);
#3920=CIRCLE('',#10116,0.243053047864041);
#3921=CIRCLE('',#10118,0.980948);
#3922=CIRCLE('',#10119,0.243053047864041);
#3923=CIRCLE('',#10121,0.243053047864041);
#3924=CIRCLE('',#10123,0.980948);
#3925=CIRCLE('',#10124,0.243053047864041);
#3926=CIRCLE('',#10126,0.243053047864041);
#3927=CIRCLE('',#10128,0.980948);
#3928=CIRCLE('',#10129,0.243053047864041);
#3929=CIRCLE('',#10131,0.243053047864041);
#3930=CIRCLE('',#10133,0.980948);
#3931=CIRCLE('',#10134,0.243053047864041);
#3932=CIRCLE('',#10136,0.243053047864041);
#3933=CIRCLE('',#10138,0.980948);
#3934=CIRCLE('',#10139,0.243053047864041);
#3935=CIRCLE('',#10141,0.243053047864041);
#3936=CIRCLE('',#10143,0.980948);
#3937=CIRCLE('',#10144,0.980948);
#3938=CIRCLE('',#10145,0.980948);
#3939=CIRCLE('',#10147,0.243053047864041);
#3940=CIRCLE('',#10149,0.243053047864041);
#4589=VERTEX_POINT('',#15638);
#4590=VERTEX_POINT('',#15639);
#4591=VERTEX_POINT('',#15662);
#4592=VERTEX_POINT('',#15664);
#4593=VERTEX_POINT('',#15689);
#4594=VERTEX_POINT('',#15691);
#4595=VERTEX_POINT('',#15714);
#4596=VERTEX_POINT('',#15716);
#4597=VERTEX_POINT('',#15739);
#4598=VERTEX_POINT('',#15741);
#4599=VERTEX_POINT('',#15754);
#4600=VERTEX_POINT('',#15757);
#4601=VERTEX_POINT('',#15770);
#4602=VERTEX_POINT('',#15772);
#4603=VERTEX_POINT('',#15795);
#4604=VERTEX_POINT('',#15797);
#4605=VERTEX_POINT('',#15820);
#4606=VERTEX_POINT('',#15822);
#4607=VERTEX_POINT('',#15845);
#4608=VERTEX_POINT('',#15847);
#4609=VERTEX_POINT('',#15872);
#4610=VERTEX_POINT('',#15876);
#4611=VERTEX_POINT('',#15901);
#4612=VERTEX_POINT('',#15905);
#4613=VERTEX_POINT('',#15930);
#4614=VERTEX_POINT('',#15934);
#4615=VERTEX_POINT('',#15935);
#4616=VERTEX_POINT('',#15962);
#4617=VERTEX_POINT('',#15966);
#4618=VERTEX_POINT('',#15991);
#4619=VERTEX_POINT('',#15995);
#4620=VERTEX_POINT('',#16020);
#4621=VERTEX_POINT('',#16024);
#4622=VERTEX_POINT('',#16049);
#4623=VERTEX_POINT('',#16052);
#4624=VERTEX_POINT('',#16054);
#5579=EDGE_CURVE('',#4589,#4590,#420,.T.);
#5580=EDGE_CURVE('',#4591,#4589,#3907,.T.);
#5581=EDGE_CURVE('',#4592,#4591,#421,.T.);
#5582=EDGE_CURVE('',#4590,#4592,#3908,.T.);
#5583=EDGE_CURVE('',#4593,#4591,#3909,.T.);
#5584=EDGE_CURVE('',#4593,#4594,#422,.T.);
#5585=EDGE_CURVE('',#4595,#4594,#3910,.T.);
#5586=EDGE_CURVE('',#4595,#4596,#423,.T.);
#5587=EDGE_CURVE('',#4597,#4596,#3911,.T.);
#5588=EDGE_CURVE('',#4597,#4598,#424,.T.);
#5589=EDGE_CURVE('',#4598,#4599,#2970,.T.);
#5590=EDGE_CURVE('',#4599,#4599,#3912,.T.);
#5591=EDGE_CURVE('',#4598,#4600,#425,.T.);
#5592=EDGE_CURVE('',#4601,#4600,#3913,.T.);
#5593=EDGE_CURVE('',#4601,#4602,#426,.T.);
#5594=EDGE_CURVE('',#4603,#4602,#3914,.T.);
#5595=EDGE_CURVE('',#4603,#4604,#427,.T.);
#5596=EDGE_CURVE('',#4605,#4604,#3915,.T.);
#5597=EDGE_CURVE('',#4605,#4606,#428,.T.);
#5598=EDGE_CURVE('',#4607,#4606,#3916,.T.);
#5599=EDGE_CURVE('',#4607,#4608,#429,.T.);
#5600=EDGE_CURVE('',#4592,#4608,#3917,.T.);
#5601=EDGE_CURVE('',#4589,#4609,#3918,.T.);
#5602=EDGE_CURVE('',#4609,#4593,#3919,.T.);
#5603=EDGE_CURVE('',#4610,#4609,#430,.T.);
#5604=EDGE_CURVE('',#4594,#4610,#3920,.T.);
#5605=EDGE_CURVE('',#4610,#4611,#3921,.T.);
#5606=EDGE_CURVE('',#4611,#4595,#3922,.T.);
#5607=EDGE_CURVE('',#4612,#4611,#431,.T.);
#5608=EDGE_CURVE('',#4596,#4612,#3923,.T.);
#5609=EDGE_CURVE('',#4612,#4613,#3924,.T.);
#5610=EDGE_CURVE('',#4613,#4597,#3925,.T.);
#5611=EDGE_CURVE('',#4614,#4615,#432,.T.);
#5612=EDGE_CURVE('',#4600,#4614,#3926,.T.);
#5613=EDGE_CURVE('',#4615,#4613,#433,.T.);
#5614=EDGE_CURVE('',#4614,#4616,#3927,.T.);
#5615=EDGE_CURVE('',#4616,#4601,#3928,.T.);
#5616=EDGE_CURVE('',#4617,#4616,#434,.T.);
#5617=EDGE_CURVE('',#4602,#4617,#3929,.T.);
#5618=EDGE_CURVE('',#4617,#4618,#3930,.T.);
#5619=EDGE_CURVE('',#4618,#4603,#3931,.T.);
#5620=EDGE_CURVE('',#4619,#4618,#435,.T.);
#5621=EDGE_CURVE('',#4604,#4619,#3932,.T.);
#5622=EDGE_CURVE('',#4619,#4620,#3933,.T.);
#5623=EDGE_CURVE('',#4620,#4605,#3934,.T.);
#5624=EDGE_CURVE('',#4621,#4620,#436,.T.);
#5625=EDGE_CURVE('',#4606,#4621,#3935,.T.);
#5626=EDGE_CURVE('',#4622,#4622,#3936,.T.);
#5627=EDGE_CURVE('',#4622,#4615,#2971,.T.);
#5628=EDGE_CURVE('',#4623,#4590,#3937,.T.);
#5629=EDGE_CURVE('',#4623,#4624,#437,.T.);
#5630=EDGE_CURVE('',#4621,#4624,#3938,.T.);
#5631=EDGE_CURVE('',#4608,#4623,#3939,.T.);
#5632=EDGE_CURVE('',#4624,#4607,#3940,.T.);
#7537=ORIENTED_EDGE('',*,*,#5579,.F.);
#7538=ORIENTED_EDGE('',*,*,#5580,.F.);
#7539=ORIENTED_EDGE('',*,*,#5581,.F.);
#7540=ORIENTED_EDGE('',*,*,#5582,.F.);
#7541=ORIENTED_EDGE('',*,*,#5581,.T.);
#7542=ORIENTED_EDGE('',*,*,#5583,.F.);
#7543=ORIENTED_EDGE('',*,*,#5584,.T.);
#7544=ORIENTED_EDGE('',*,*,#5585,.F.);
#7545=ORIENTED_EDGE('',*,*,#5586,.T.);
#7546=ORIENTED_EDGE('',*,*,#5587,.F.);
#7547=ORIENTED_EDGE('',*,*,#5588,.T.);
#7548=ORIENTED_EDGE('',*,*,#5589,.T.);
#7549=ORIENTED_EDGE('',*,*,#5590,.F.);
#7550=ORIENTED_EDGE('',*,*,#5589,.F.);
#7551=ORIENTED_EDGE('',*,*,#5591,.T.);
#7552=ORIENTED_EDGE('',*,*,#5592,.F.);
#7553=ORIENTED_EDGE('',*,*,#5593,.T.);
#7554=ORIENTED_EDGE('',*,*,#5594,.F.);
#7555=ORIENTED_EDGE('',*,*,#5595,.T.);
#7556=ORIENTED_EDGE('',*,*,#5596,.F.);
#7557=ORIENTED_EDGE('',*,*,#5597,.T.);
#7558=ORIENTED_EDGE('',*,*,#5598,.F.);
#7559=ORIENTED_EDGE('',*,*,#5599,.T.);
#7560=ORIENTED_EDGE('',*,*,#5600,.F.);
#7561=ORIENTED_EDGE('',*,*,#5580,.T.);
#7562=ORIENTED_EDGE('',*,*,#5601,.T.);
#7563=ORIENTED_EDGE('',*,*,#5602,.T.);
#7564=ORIENTED_EDGE('',*,*,#5583,.T.);
#7565=ORIENTED_EDGE('',*,*,#5603,.F.);
#7566=ORIENTED_EDGE('',*,*,#5604,.F.);
#7567=ORIENTED_EDGE('',*,*,#5584,.F.);
#7568=ORIENTED_EDGE('',*,*,#5602,.F.);
#7569=ORIENTED_EDGE('',*,*,#5604,.T.);
#7570=ORIENTED_EDGE('',*,*,#5605,.T.);
#7571=ORIENTED_EDGE('',*,*,#5606,.T.);
#7572=ORIENTED_EDGE('',*,*,#5585,.T.);
#7573=ORIENTED_EDGE('',*,*,#5607,.F.);
#7574=ORIENTED_EDGE('',*,*,#5608,.F.);
#7575=ORIENTED_EDGE('',*,*,#5586,.F.);
#7576=ORIENTED_EDGE('',*,*,#5606,.F.);
#7577=ORIENTED_EDGE('',*,*,#5608,.T.);
#7578=ORIENTED_EDGE('',*,*,#5609,.T.);
#7579=ORIENTED_EDGE('',*,*,#5610,.T.);
#7580=ORIENTED_EDGE('',*,*,#5587,.T.);
#7581=ORIENTED_EDGE('',*,*,#5611,.F.);
#7582=ORIENTED_EDGE('',*,*,#5612,.F.);
#7583=ORIENTED_EDGE('',*,*,#5591,.F.);
#7584=ORIENTED_EDGE('',*,*,#5588,.F.);
#7585=ORIENTED_EDGE('',*,*,#5610,.F.);
#7586=ORIENTED_EDGE('',*,*,#5613,.F.);
#7587=ORIENTED_EDGE('',*,*,#5612,.T.);
#7588=ORIENTED_EDGE('',*,*,#5614,.T.);
#7589=ORIENTED_EDGE('',*,*,#5615,.T.);
#7590=ORIENTED_EDGE('',*,*,#5592,.T.);
#7591=ORIENTED_EDGE('',*,*,#5616,.F.);
#7592=ORIENTED_EDGE('',*,*,#5617,.F.);
#7593=ORIENTED_EDGE('',*,*,#5593,.F.);
#7594=ORIENTED_EDGE('',*,*,#5615,.F.);
#7595=ORIENTED_EDGE('',*,*,#5617,.T.);
#7596=ORIENTED_EDGE('',*,*,#5618,.T.);
#7597=ORIENTED_EDGE('',*,*,#5619,.T.);
#7598=ORIENTED_EDGE('',*,*,#5594,.T.);
#7599=ORIENTED_EDGE('',*,*,#5620,.F.);
#7600=ORIENTED_EDGE('',*,*,#5621,.F.);
#7601=ORIENTED_EDGE('',*,*,#5595,.F.);
#7602=ORIENTED_EDGE('',*,*,#5619,.F.);
#7603=ORIENTED_EDGE('',*,*,#5621,.T.);
#7604=ORIENTED_EDGE('',*,*,#5622,.T.);
#7605=ORIENTED_EDGE('',*,*,#5623,.T.);
#7606=ORIENTED_EDGE('',*,*,#5596,.T.);
#7607=ORIENTED_EDGE('',*,*,#5597,.F.);
#7608=ORIENTED_EDGE('',*,*,#5623,.F.);
#7609=ORIENTED_EDGE('',*,*,#5624,.F.);
#7610=ORIENTED_EDGE('',*,*,#5625,.F.);
#7611=ORIENTED_EDGE('',*,*,#5626,.F.);
#7612=ORIENTED_EDGE('',*,*,#5627,.T.);
#7613=ORIENTED_EDGE('',*,*,#5613,.T.);
#7614=ORIENTED_EDGE('',*,*,#5609,.F.);
#7615=ORIENTED_EDGE('',*,*,#5607,.T.);
#7616=ORIENTED_EDGE('',*,*,#5605,.F.);
#7617=ORIENTED_EDGE('',*,*,#5603,.T.);
#7618=ORIENTED_EDGE('',*,*,#5601,.F.);
#7619=ORIENTED_EDGE('',*,*,#5579,.T.);
#7620=ORIENTED_EDGE('',*,*,#5628,.F.);
#7621=ORIENTED_EDGE('',*,*,#5629,.T.);
#7622=ORIENTED_EDGE('',*,*,#5630,.F.);
#7623=ORIENTED_EDGE('',*,*,#5624,.T.);
#7624=ORIENTED_EDGE('',*,*,#5622,.F.);
#7625=ORIENTED_EDGE('',*,*,#5620,.T.);
#7626=ORIENTED_EDGE('',*,*,#5618,.F.);
#7627=ORIENTED_EDGE('',*,*,#5616,.T.);
#7628=ORIENTED_EDGE('',*,*,#5614,.F.);
#7629=ORIENTED_EDGE('',*,*,#5611,.T.);
#7630=ORIENTED_EDGE('',*,*,#5627,.F.);
#7631=ORIENTED_EDGE('',*,*,#5582,.T.);
#7632=ORIENTED_EDGE('',*,*,#5600,.T.);
#7633=ORIENTED_EDGE('',*,*,#5631,.T.);
#7634=ORIENTED_EDGE('',*,*,#5628,.T.);
#7635=ORIENTED_EDGE('',*,*,#5599,.F.);
#7636=ORIENTED_EDGE('',*,*,#5632,.F.);
#7637=ORIENTED_EDGE('',*,*,#5629,.F.);
#7638=ORIENTED_EDGE('',*,*,#5631,.F.);
#7639=ORIENTED_EDGE('',*,*,#5590,.T.);
#7640=ORIENTED_EDGE('',*,*,#5626,.T.);
#7641=ORIENTED_EDGE('',*,*,#5625,.T.);
#7642=ORIENTED_EDGE('',*,*,#5630,.T.);
#7643=ORIENTED_EDGE('',*,*,#5632,.T.);
#7644=ORIENTED_EDGE('',*,*,#5598,.T.);
#7847=CYLINDRICAL_SURFACE('',#10102,1.019052);
#7848=CYLINDRICAL_SURFACE('',#10142,0.980948);
#8331=ADVANCED_FACE('',(#1728),#464,.F.);
#8332=ADVANCED_FACE('',(#1729),#7847,.T.);
#8333=ADVANCED_FACE('',(#1730),#1237,.T.);
#8334=ADVANCED_FACE('',(#1731),#465,.F.);
#8335=ADVANCED_FACE('',(#1732),#1238,.T.);
#8336=ADVANCED_FACE('',(#1733),#466,.F.);
#8337=ADVANCED_FACE('',(#1734),#1239,.T.);
#8338=ADVANCED_FACE('',(#1735),#467,.F.);
#8339=ADVANCED_FACE('',(#1736),#1240,.T.);
#8340=ADVANCED_FACE('',(#1737),#468,.F.);
#8341=ADVANCED_FACE('',(#1738),#1241,.T.);
#8342=ADVANCED_FACE('',(#1739),#469,.F.);
#8343=ADVANCED_FACE('',(#1740),#1242,.T.);
#8344=ADVANCED_FACE('',(#1741),#470,.F.);
#8345=ADVANCED_FACE('',(#1742),#7848,.F.);
#8346=ADVANCED_FACE('',(#1743),#1243,.T.);
#8347=ADVANCED_FACE('',(#1744),#471,.F.);
#8348=ADVANCED_FACE('',(#1745,#985),#1244,.T.);
#8349=ADVANCED_FACE('',(#1746),#1245,.T.);
#8431=CLOSED_SHELL('',(#8331,#8332,#8333,#8334,#8335,#8336,#8337,#8338,
#8339,#8340,#8341,#8342,#8343,#8344,#8345,#8346,#8347,#8348,#8349));
#10098=AXIS2_PLACEMENT_3D('',#15636,#12793,#12794);
#10099=AXIS2_PLACEMENT_3D('',#15637,#12795,#12796);
#10100=AXIS2_PLACEMENT_3D('',#15663,#12797,#12798);
#10101=AXIS2_PLACEMENT_3D('',#15687,#12799,#12800);
#10102=AXIS2_PLACEMENT_3D('',#15688,#12801,#12802);
#10103=AXIS2_PLACEMENT_3D('',#15690,#12803,#12804);
#10104=AXIS2_PLACEMENT_3D('',#15715,#12805,#12806);
#10105=AXIS2_PLACEMENT_3D('',#15740,#12807,#12808);
#10106=AXIS2_PLACEMENT_3D('',#15756,#12810,#12811);
#10107=AXIS2_PLACEMENT_3D('',#15771,#12812,#12813);
#10108=AXIS2_PLACEMENT_3D('',#15796,#12814,#12815);
#10109=AXIS2_PLACEMENT_3D('',#15821,#12816,#12817);
#10110=AXIS2_PLACEMENT_3D('',#15846,#12818,#12819);
#10111=AXIS2_PLACEMENT_3D('',#15870,#12820,#12821);
#10112=AXIS2_PLACEMENT_3D('',#15871,#12822,#12823);
#10113=AXIS2_PLACEMENT_3D('',#15873,#12824,#12825);
#10114=AXIS2_PLACEMENT_3D('',#15874,#12826,#12827);
#10115=AXIS2_PLACEMENT_3D('',#15875,#12828,#12829);
#10116=AXIS2_PLACEMENT_3D('',#15899,#12830,#12831);
#10117=AXIS2_PLACEMENT_3D('',#15900,#12832,#12833);
#10118=AXIS2_PLACEMENT_3D('',#15902,#12834,#12835);
#10119=AXIS2_PLACEMENT_3D('',#15903,#12836,#12837);
#10120=AXIS2_PLACEMENT_3D('',#15904,#12838,#12839);
#10121=AXIS2_PLACEMENT_3D('',#15928,#12840,#12841);
#10122=AXIS2_PLACEMENT_3D('',#15929,#12842,#12843);
#10123=AXIS2_PLACEMENT_3D('',#15931,#12844,#12845);
#10124=AXIS2_PLACEMENT_3D('',#15932,#12846,#12847);
#10125=AXIS2_PLACEMENT_3D('',#15933,#12848,#12849);
#10126=AXIS2_PLACEMENT_3D('',#15948,#12850,#12851);
#10127=AXIS2_PLACEMENT_3D('',#15961,#12852,#12853);
#10128=AXIS2_PLACEMENT_3D('',#15963,#12854,#12855);
#10129=AXIS2_PLACEMENT_3D('',#15964,#12856,#12857);
#10130=AXIS2_PLACEMENT_3D('',#15965,#12858,#12859);
#10131=AXIS2_PLACEMENT_3D('',#15989,#12860,#12861);
#10132=AXIS2_PLACEMENT_3D('',#15990,#12862,#12863);
#10133=AXIS2_PLACEMENT_3D('',#15992,#12864,#12865);
#10134=AXIS2_PLACEMENT_3D('',#15993,#12866,#12867);
#10135=AXIS2_PLACEMENT_3D('',#15994,#12868,#12869);
#10136=AXIS2_PLACEMENT_3D('',#16018,#12870,#12871);
#10137=AXIS2_PLACEMENT_3D('',#16019,#12872,#12873);
#10138=AXIS2_PLACEMENT_3D('',#16021,#12874,#12875);
#10139=AXIS2_PLACEMENT_3D('',#16022,#12876,#12877);
#10140=AXIS2_PLACEMENT_3D('',#16023,#12878,#12879);
#10141=AXIS2_PLACEMENT_3D('',#16047,#12880,#12881);
#10142=AXIS2_PLACEMENT_3D('',#16048,#12882,#12883);
#10143=AXIS2_PLACEMENT_3D('',#16050,#12884,#12885);
#10144=AXIS2_PLACEMENT_3D('',#16053,#12887,#12888);
#10145=AXIS2_PLACEMENT_3D('',#16077,#12889,#12890);
#10146=AXIS2_PLACEMENT_3D('',#16078,#12891,#12892);
#10147=AXIS2_PLACEMENT_3D('',#16079,#12893,#12894);
#10148=AXIS2_PLACEMENT_3D('',#16080,#12895,#12896);
#10149=AXIS2_PLACEMENT_3D('',#16081,#12897,#12898);
#10150=AXIS2_PLACEMENT_3D('',#16082,#12899,#12900);
#10151=AXIS2_PLACEMENT_3D('',#16083,#12901,#12902);
#12793=DIRECTION('axis',(0.,0.,1.));
#12794=DIRECTION('refdir',(1.,0.,0.));
#12795=DIRECTION('center_axis',(0.,0.,1.));
#12796=DIRECTION('ref_axis',(1.,0.,0.));
#12797=DIRECTION('center_axis',(0.,-1.,0.));
#12798=DIRECTION('ref_axis',(0.,0.,-1.));
#12799=DIRECTION('center_axis',(0.,-1.,0.));
#12800=DIRECTION('ref_axis',(0.,0.,-1.));
#12801=DIRECTION('center_axis',(0.,1.,0.));
#12802=DIRECTION('ref_axis',(1.,0.,0.));
#12803=DIRECTION('center_axis',(0.,1.,0.));
#12804=DIRECTION('ref_axis',(1.,0.,0.));
#12805=DIRECTION('center_axis',(0.,1.,0.));
#12806=DIRECTION('ref_axis',(1.,0.,0.));
#12807=DIRECTION('center_axis',(0.,1.,0.));
#12808=DIRECTION('ref_axis',(1.,0.,0.));
#12809=DIRECTION('',(0.,-1.,0.));
#12810=DIRECTION('center_axis',(0.,-1.,0.));
#12811=DIRECTION('ref_axis',(1.,0.,0.));
#12812=DIRECTION('center_axis',(0.,1.,0.));
#12813=DIRECTION('ref_axis',(1.,0.,0.));
#12814=DIRECTION('center_axis',(0.,1.,0.));
#12815=DIRECTION('ref_axis',(1.,0.,0.));
#12816=DIRECTION('center_axis',(0.,1.,0.));
#12817=DIRECTION('ref_axis',(1.,0.,0.));
#12818=DIRECTION('center_axis',(0.,1.,0.));
#12819=DIRECTION('ref_axis',(1.,0.,0.));
#12820=DIRECTION('center_axis',(0.,1.,0.));
#12821=DIRECTION('ref_axis',(1.,0.,0.));
#12822=DIRECTION('center_axis',(0.,1.,0.));
#12823=DIRECTION('ref_axis',(1.,0.,0.));
#12824=DIRECTION('center_axis',(0.,-1.,0.));
#12825=DIRECTION('ref_axis',(1.,0.,0.));
#12826=DIRECTION('center_axis',(0.,-1.,0.));
#12827=DIRECTION('ref_axis',(0.,0.,-1.));
#12828=DIRECTION('center_axis',(6.12323399573677E-17,0.,1.));
#12829=DIRECTION('ref_axis',(1.,0.,0.));
#12830=DIRECTION('center_axis',(0.,-1.,0.));
#12831=DIRECTION('ref_axis',(0.,0.,-1.));
#12832=DIRECTION('center_axis',(0.,1.,0.));
#12833=DIRECTION('ref_axis',(1.,0.,0.));
#12834=DIRECTION('center_axis',(0.,-1.,0.));
#12835=DIRECTION('ref_axis',(1.,0.,0.));
#12836=DIRECTION('center_axis',(0.,-1.,0.));
#12837=DIRECTION('ref_axis',(0.,0.,-1.));
#12838=DIRECTION('center_axis',(0.,0.,1.));
#12839=DIRECTION('ref_axis',(1.,0.,0.));
#12840=DIRECTION('center_axis',(0.,-1.,0.));
#12841=DIRECTION('ref_axis',(0.,0.,-1.));
#12842=DIRECTION('center_axis',(0.,1.,0.));
#12843=DIRECTION('ref_axis',(1.,0.,0.));
#12844=DIRECTION('center_axis',(0.,-1.,0.));
#12845=DIRECTION('ref_axis',(1.,0.,0.));
#12846=DIRECTION('center_axis',(0.,-1.,0.));
#12847=DIRECTION('ref_axis',(0.,0.,-1.));
#12848=DIRECTION('center_axis',(0.,0.,1.));
#12849=DIRECTION('ref_axis',(1.,0.,0.));
#12850=DIRECTION('center_axis',(0.,-1.,0.));
#12851=DIRECTION('ref_axis',(0.,0.,-1.));
#12852=DIRECTION('center_axis',(0.,1.,0.));
#12853=DIRECTION('ref_axis',(1.,0.,0.));
#12854=DIRECTION('center_axis',(0.,-1.,0.));
#12855=DIRECTION('ref_axis',(1.,0.,0.));
#12856=DIRECTION('center_axis',(0.,-1.,0.));
#12857=DIRECTION('ref_axis',(0.,0.,-1.));
#12858=DIRECTION('center_axis',(0.,0.,1.));
#12859=DIRECTION('ref_axis',(1.,0.,0.));
#12860=DIRECTION('center_axis',(0.,-1.,0.));
#12861=DIRECTION('ref_axis',(0.,0.,-1.));
#12862=DIRECTION('center_axis',(0.,1.,0.));
#12863=DIRECTION('ref_axis',(1.,0.,0.));
#12864=DIRECTION('center_axis',(0.,-1.,0.));
#12865=DIRECTION('ref_axis',(1.,0.,0.));
#12866=DIRECTION('center_axis',(0.,-1.,0.));
#12867=DIRECTION('ref_axis',(0.,0.,-1.));
#12868=DIRECTION('center_axis',(6.12323399573676E-17,0.,1.));
#12869=DIRECTION('ref_axis',(1.,0.,0.));
#12870=DIRECTION('center_axis',(0.,-1.,0.));
#12871=DIRECTION('ref_axis',(0.,0.,-1.));
#12872=DIRECTION('center_axis',(0.,1.,0.));
#12873=DIRECTION('ref_axis',(1.,0.,0.));
#12874=DIRECTION('center_axis',(0.,-1.,0.));
#12875=DIRECTION('ref_axis',(1.,0.,0.));
#12876=DIRECTION('center_axis',(0.,-1.,0.));
#12877=DIRECTION('ref_axis',(0.,0.,-1.));
#12878=DIRECTION('center_axis',(0.,0.,1.));
#12879=DIRECTION('ref_axis',(1.,0.,0.));
#12880=DIRECTION('center_axis',(0.,-1.,0.));
#12881=DIRECTION('ref_axis',(0.,0.,-1.));
#12882=DIRECTION('center_axis',(0.,1.,0.));
#12883=DIRECTION('ref_axis',(1.,0.,0.));
#12884=DIRECTION('center_axis',(0.,1.,0.));
#12885=DIRECTION('ref_axis',(1.,0.,0.));
#12886=DIRECTION('',(0.,1.,0.));
#12887=DIRECTION('center_axis',(0.,-1.,0.));
#12888=DIRECTION('ref_axis',(1.,0.,0.));
#12889=DIRECTION('center_axis',(0.,-1.,0.));
#12890=DIRECTION('ref_axis',(1.,0.,0.));
#12891=DIRECTION('center_axis',(0.,1.,0.));
#12892=DIRECTION('ref_axis',(1.,0.,0.));
#12893=DIRECTION('center_axis',(0.,-1.,0.));
#12894=DIRECTION('ref_axis',(0.,0.,-1.));
#12895=DIRECTION('center_axis',(0.,0.,1.));
#12896=DIRECTION('ref_axis',(1.,0.,0.));
#12897=DIRECTION('center_axis',(0.,-1.,0.));
#12898=DIRECTION('ref_axis',(0.,0.,-1.));
#12899=DIRECTION('center_axis',(0.,-1.,0.));
#12900=DIRECTION('ref_axis',(-1.,0.,0.));
#12901=DIRECTION('center_axis',(0.,1.,0.));
#12902=DIRECTION('ref_axis',(1.,0.,0.));
#15636=CARTESIAN_POINT('',(0.,0.,0.));
#15637=CARTESIAN_POINT('Origin',(0.707106781186547,0.,0.707106781186548));
#15638=CARTESIAN_POINT('',(0.504455939115715,-0.04763,0.841298510752802));
#15639=CARTESIAN_POINT('',(0.841298510752802,-0.04763,0.504455939115715));
#15640=CARTESIAN_POINT('Ctrl Pts',(0.504455939115715,-0.04763,0.841298510752802));
#15641=CARTESIAN_POINT('Ctrl Pts',(0.508899795931835,-0.0740444353928835,
0.838633903678357));
#15642=CARTESIAN_POINT('Ctrl Pts',(0.517157748491652,-0.0999305678883309,
0.833661031856294));
#15643=CARTESIAN_POINT('Ctrl Pts',(0.537715343527944,-0.142345102874864,
0.820511285096538));
#15644=CARTESIAN_POINT('Ctrl Pts',(0.548874290046456,-0.159766064500479,
0.813159949759));
#15645=CARTESIAN_POINT('Ctrl Pts',(0.573915184558107,-0.190326085855194,
0.795684265985089));
#15646=CARTESIAN_POINT('Ctrl Pts',(0.587792702767295,-0.203463743702801,
0.78555112003688));
#15647=CARTESIAN_POINT('Ctrl Pts',(0.615966552324775,-0.224161999508995,
0.763642258217233));
#15648=CARTESIAN_POINT('Ctrl Pts',(0.631684198665438,-0.232861760990032,
0.750785745543687));
#15649=CARTESIAN_POINT('Ctrl Pts',(0.663382628119203,-0.244251601209411,
0.722929908501543));
#15650=CARTESIAN_POINT('Ctrl Pts',(0.679352081686668,-0.246942143572133,
0.707917883896095));
#15651=CARTESIAN_POINT('Ctrl Pts',(0.707917883896095,-0.246942143572133,
0.679352081686668));
#15652=CARTESIAN_POINT('Ctrl Pts',(0.722929908501543,-0.244251601209411,
0.663382628119203));
#15653=CARTESIAN_POINT('Ctrl Pts',(0.750785745543687,-0.232861760990032,
0.631684198665439));
#15654=CARTESIAN_POINT('Ctrl Pts',(0.763642258217232,-0.224161999508995,
0.615966552324775));
#15655=CARTESIAN_POINT('Ctrl Pts',(0.78555112003688,-0.203463743702801,
0.587792702767295));
#15656=CARTESIAN_POINT('Ctrl Pts',(0.795684265985088,-0.190326085855194,
0.573915184558108));
#15657=CARTESIAN_POINT('Ctrl Pts',(0.813159949759,-0.15976606450048,0.548874290046456));
#15658=CARTESIAN_POINT('Ctrl Pts',(0.820511285096538,-0.142345102874864,
0.537715343527944));
#15659=CARTESIAN_POINT('Ctrl Pts',(0.833661031856294,-0.099930567888331,
0.517157748491653));
#15660=CARTESIAN_POINT('Ctrl Pts',(0.838633903678357,-0.0740444353928835,
0.508899795931835));
#15661=CARTESIAN_POINT('Ctrl Pts',(0.841298510752801,-0.0476299999999999,
0.504455939115715));
#15662=CARTESIAN_POINT('',(0.528110872004958,-0.04763,0.871530771444223));
#15663=CARTESIAN_POINT('Origin',(0.707106781186547,-0.04763,0.707106781186548));
#15664=CARTESIAN_POINT('',(0.871530771444223,-0.04763,0.528110872004959));
#15665=CARTESIAN_POINT('Ctrl Pts',(0.871530771444223,-0.0476300000000001,
0.528110872004958));
#15666=CARTESIAN_POINT('Ctrl Pts',(0.87014664509073,-0.0609922781173483,
0.530395067942936));
#15667=CARTESIAN_POINT('Ctrl Pts',(0.868149331745851,-0.0742967091364493,
0.533674141594226));
#15668=CARTESIAN_POINT('Ctrl Pts',(0.85981294420286,-0.115492077056649,
0.54708917182331));
#15669=CARTESIAN_POINT('Ctrl Pts',(0.850993704737257,-0.141695629206859,
0.560922177770136));
#15670=CARTESIAN_POINT('Ctrl Pts',(0.830754510485543,-0.181890537957859,
0.590422647829571));
#15671=CARTESIAN_POINT('Ctrl Pts',(0.816896541396381,-0.201072148666545,
0.609616703125488));
#15672=CARTESIAN_POINT('Ctrl Pts',(0.792310597819928,-0.223955109275652,
0.641117951819998));
#15673=CARTESIAN_POINT('Ctrl Pts',(0.779109323683612,-0.232742381310829,
0.657208095763053));
#15674=CARTESIAN_POINT('Ctrl Pts',(0.750552691816206,-0.244234834628584,
0.68964083160521));
#15675=CARTESIAN_POINT('Ctrl Pts',(0.735185187071673,-0.246942143572133,
0.705971972091755));
#15676=CARTESIAN_POINT('Ctrl Pts',(0.705971972091754,-0.246942143572133,
0.735185187071673));
#15677=CARTESIAN_POINT('Ctrl Pts',(0.689640831605209,-0.244234834628584,
0.750552691816206));
#15678=CARTESIAN_POINT('Ctrl Pts',(0.657208095763052,-0.232742381310829,
0.779109323683612));
#15679=CARTESIAN_POINT('Ctrl Pts',(0.641117951819998,-0.223955109275652,
0.792310597819928));
#15680=CARTESIAN_POINT('Ctrl Pts',(0.609616703125487,-0.201072148666545,
0.816896541396382));
#15681=CARTESIAN_POINT('Ctrl Pts',(0.590422647829571,-0.181890537957858,
0.830754510485544));
#15682=CARTESIAN_POINT('Ctrl Pts',(0.560922177770135,-0.141695629206858,
0.850993704737257));
#15683=CARTESIAN_POINT('Ctrl Pts',(0.547089171823309,-0.115492077056649,
0.859812944202861));
#15684=CARTESIAN_POINT('Ctrl Pts',(0.533674141594226,-0.0742967091364491,
0.868149331745852));
#15685=CARTESIAN_POINT('Ctrl Pts',(0.530395067942936,-0.0609922781173483,
0.870146645090731));
#15686=CARTESIAN_POINT('Ctrl Pts',(0.528110872004958,-0.0476300000000001,
0.871530771444223));
#15687=CARTESIAN_POINT('Origin',(0.707106781186547,-0.04763,0.707106781186548));
#15688=CARTESIAN_POINT('Origin',(0.,-0.166705,0.));
#15689=CARTESIAN_POINT('',(0.242834539687906,-0.04763,0.989696097314));
#15690=CARTESIAN_POINT('Origin',(0.,-0.04763,0.));
#15691=CARTESIAN_POINT('',(-0.242834539687907,-0.04763,0.989696097314));
#15692=CARTESIAN_POINT('Ctrl Pts',(0.242834539687906,-0.04763,0.989696097314));
#15693=CARTESIAN_POINT('Ctrl Pts',(0.24024064412003,-0.0609922781173483,
0.990332542620729));
#15694=CARTESIAN_POINT('Ctrl Pts',(0.236509675094874,-0.0742967091364492,
0.991238884025248));
#15695=CARTESIAN_POINT('Ctrl Pts',(0.221129100087819,-0.115492077056649,
0.994830026707808));
#15696=CARTESIAN_POINT('Ctrl Pts',(0.205111543747588,-0.141695629206859,
0.998375294985966));
#15697=CARTESIAN_POINT('Ctrl Pts',(0.169940289819232,-0.181890537957859,
1.00492400591205));
#15698=CARTESIAN_POINT('Ctrl Pts',(0.1465689792446,-0.201072148666545,1.00869718865384));
#15699=CARTESIAN_POINT('Ctrl Pts',(0.106909345252087,-0.223955109275652,
1.01358704779679));
#15700=CARTESIAN_POINT('Ctrl Pts',(0.0861971848975941,-0.232742381310829,
1.0156297872271));
#15701=CARTESIAN_POINT('Ctrl Pts',(0.0430711894098822,-0.244234834628584,
1.01837060663223));
#15702=CARTESIAN_POINT('Ctrl Pts',(0.0206568624125605,-0.246942143572133,
1.019052));
#15703=CARTESIAN_POINT('Ctrl Pts',(-0.0206568624125608,-0.246942143572133,
1.019052));
#15704=CARTESIAN_POINT('Ctrl Pts',(-0.0430711894098825,-0.244234834628584,
1.01837060663223));
#15705=CARTESIAN_POINT('Ctrl Pts',(-0.0861971848975943,-0.232742381310829,
1.0156297872271));
#15706=CARTESIAN_POINT('Ctrl Pts',(-0.106909345252088,-0.223955109275652,
1.01358704779679));
#15707=CARTESIAN_POINT('Ctrl Pts',(-0.1465689792446,-0.201072148666545,
1.00869718865384));
#15708=CARTESIAN_POINT('Ctrl Pts',(-0.169940289819232,-0.181890537957859,
1.00492400591205));
#15709=CARTESIAN_POINT('Ctrl Pts',(-0.205111543747588,-0.141695629206859,
0.998375294985966));
#15710=CARTESIAN_POINT('Ctrl Pts',(-0.221129100087819,-0.115492077056649,
0.994830026707808));
#15711=CARTESIAN_POINT('Ctrl Pts',(-0.236509675094875,-0.0742967091364493,
0.991238884025248));
#15712=CARTESIAN_POINT('Ctrl Pts',(-0.24024064412003,-0.0609922781173483,
0.990332542620729));
#15713=CARTESIAN_POINT('Ctrl Pts',(-0.242834539687907,-0.04763,0.989696097314));
#15714=CARTESIAN_POINT('',(-0.528110872004959,-0.04763,0.871530771444223));
#15715=CARTESIAN_POINT('Origin',(0.,-0.04763,0.));
#15716=CARTESIAN_POINT('',(-0.871530771444223,-0.04763,0.528110872004958));
#15717=CARTESIAN_POINT('Ctrl Pts',(-0.528110872004958,-0.0476300000000001,
0.871530771444223));
#15718=CARTESIAN_POINT('Ctrl Pts',(-0.530395067942936,-0.0609922781173484,
0.87014664509073));
#15719=CARTESIAN_POINT('Ctrl Pts',(-0.533674141594226,-0.0742967091364493,
0.868149331745851));
#15720=CARTESIAN_POINT('Ctrl Pts',(-0.54708917182331,-0.115492077056649,
0.85981294420286));
#15721=CARTESIAN_POINT('Ctrl Pts',(-0.560922177770136,-0.141695629206859,
0.850993704737257));
#15722=CARTESIAN_POINT('Ctrl Pts',(-0.590422647829571,-0.181890537957859,
0.830754510485543));
#15723=CARTESIAN_POINT('Ctrl Pts',(-0.609616703125488,-0.201072148666545,
0.816896541396381));
#15724=CARTESIAN_POINT('Ctrl Pts',(-0.641117951819998,-0.223955109275652,
0.792310597819928));
#15725=CARTESIAN_POINT('Ctrl Pts',(-0.657208095763053,-0.232742381310829,
0.779109323683611));
#15726=CARTESIAN_POINT('Ctrl Pts',(-0.68964083160521,-0.244234834628584,
0.750552691816205));
#15727=CARTESIAN_POINT('Ctrl Pts',(-0.705971972091755,-0.246942143572133,
0.735185187071673));
#15728=CARTESIAN_POINT('Ctrl Pts',(-0.735185187071673,-0.246942143572133,
0.705971972091754));
#15729=CARTESIAN_POINT('Ctrl Pts',(-0.750552691816206,-0.244234834628584,
0.689640831605209));
#15730=CARTESIAN_POINT('Ctrl Pts',(-0.779109323683612,-0.232742381310829,
0.657208095763052));
#15731=CARTESIAN_POINT('Ctrl Pts',(-0.792310597819928,-0.223955109275652,
0.641117951819998));
#15732=CARTESIAN_POINT('Ctrl Pts',(-0.816896541396382,-0.201072148666545,
0.609616703125487));
#15733=CARTESIAN_POINT('Ctrl Pts',(-0.830754510485544,-0.181890537957858,
0.590422647829571));
#15734=CARTESIAN_POINT('Ctrl Pts',(-0.850993704737257,-0.141695629206858,
0.560922177770135));
#15735=CARTESIAN_POINT('Ctrl Pts',(-0.859812944202861,-0.115492077056649,
0.547089171823309));
#15736=CARTESIAN_POINT('Ctrl Pts',(-0.868149331745852,-0.0742967091364491,
0.533674141594226));
#15737=CARTESIAN_POINT('Ctrl Pts',(-0.870146645090731,-0.0609922781173483,
0.530395067942936));
#15738=CARTESIAN_POINT('Ctrl Pts',(-0.871530771444223,-0.04763,0.528110872004958));
#15739=CARTESIAN_POINT('',(-0.989696097314,-0.04763,0.242834539687906));
#15740=CARTESIAN_POINT('Origin',(0.,-0.04763,0.));
#15741=CARTESIAN_POINT('',(-1.019052,-0.246942143572133,1.248489836334E-16));
#15742=CARTESIAN_POINT('Ctrl Pts',(-0.989696097314,-0.04763,0.242834539687906));
#15743=CARTESIAN_POINT('Ctrl Pts',(-0.990332542620729,-0.0609922781173483,
0.24024064412003));
#15744=CARTESIAN_POINT('Ctrl Pts',(-0.991238884025248,-0.0742967091364492,
0.236509675094874));
#15745=CARTESIAN_POINT('Ctrl Pts',(-0.994830026707808,-0.115492077056649,
0.221129100087819));
#15746=CARTESIAN_POINT('Ctrl Pts',(-0.998375294985966,-0.141695629206859,
0.205111543747588));
#15747=CARTESIAN_POINT('Ctrl Pts',(-1.00492400591205,-0.181890537957859,
0.169940289819232));
#15748=CARTESIAN_POINT('Ctrl Pts',(-1.00869718865384,-0.201072148666545,
0.1465689792446));
#15749=CARTESIAN_POINT('Ctrl Pts',(-1.01358704779679,-0.223955109275652,
0.106909345252088));
#15750=CARTESIAN_POINT('Ctrl Pts',(-1.0156297872271,-0.232742381310829,
0.0861971848975944));
#15751=CARTESIAN_POINT('Ctrl Pts',(-1.01837060663223,-0.244234834628584,
0.0430711894098825));
#15752=CARTESIAN_POINT('Ctrl Pts',(-1.019052,-0.246942143572133,0.0206568624125608));
#15753=CARTESIAN_POINT('Ctrl Pts',(-1.019052,-0.246942143572133,1.2490009027033E-16));
#15754=CARTESIAN_POINT('',(-1.019052,-0.28578,1.24797876996471E-16));
#15755=CARTESIAN_POINT('',(-1.019052,-0.166705,1.24797876996471E-16));
#15756=CARTESIAN_POINT('Origin',(0.,-0.28578,0.));
#15757=CARTESIAN_POINT('',(-0.989696097314,-0.04763,-0.242834539687906));
#15758=CARTESIAN_POINT('Ctrl Pts',(-1.019052,-0.246942143572133,1.2490009027033E-16));
#15759=CARTESIAN_POINT('Ctrl Pts',(-1.019052,-0.246942143572133,-0.0206568624125605));
#15760=CARTESIAN_POINT('Ctrl Pts',(-1.01837060663223,-0.244234834628584,
-0.0430711894098822));
#15761=CARTESIAN_POINT('Ctrl Pts',(-1.0156297872271,-0.232742381310829,
-0.0861971848975941));
#15762=CARTESIAN_POINT('Ctrl Pts',(-1.01358704779679,-0.223955109275652,
-0.106909345252087));
#15763=CARTESIAN_POINT('Ctrl Pts',(-1.00869718865384,-0.201072148666546,
-0.1465689792446));
#15764=CARTESIAN_POINT('Ctrl Pts',(-1.00492400591205,-0.181890537957859,
-0.169940289819232));
#15765=CARTESIAN_POINT('Ctrl Pts',(-0.998375294985966,-0.141695629206859,
-0.205111543747588));
#15766=CARTESIAN_POINT('Ctrl Pts',(-0.994830026707808,-0.11549207705665,
-0.221129100087819));
#15767=CARTESIAN_POINT('Ctrl Pts',(-0.991238884025248,-0.0742967091364495,
-0.236509675094874));
#15768=CARTESIAN_POINT('Ctrl Pts',(-0.990332542620729,-0.0609922781173484,
-0.24024064412003));
#15769=CARTESIAN_POINT('Ctrl Pts',(-0.989696097314,-0.0476300000000001,
-0.242834539687907));
#15770=CARTESIAN_POINT('',(-0.871530771444223,-0.04763,-0.528110872004958));
#15771=CARTESIAN_POINT('Origin',(0.,-0.04763,0.));
#15772=CARTESIAN_POINT('',(-0.528110872004958,-0.04763,-0.871530771444223));
#15773=CARTESIAN_POINT('Ctrl Pts',(-0.871530771444223,-0.0476300000000001,
-0.528110872004958));
#15774=CARTESIAN_POINT('Ctrl Pts',(-0.87014664509073,-0.0609922781173484,
-0.530395067942936));
#15775=CARTESIAN_POINT('Ctrl Pts',(-0.868149331745851,-0.0742967091364494,
-0.533674141594226));
#15776=CARTESIAN_POINT('Ctrl Pts',(-0.85981294420286,-0.115492077056649,
-0.54708917182331));
#15777=CARTESIAN_POINT('Ctrl Pts',(-0.850993704737257,-0.141695629206859,
-0.560922177770136));
#15778=CARTESIAN_POINT('Ctrl Pts',(-0.830754510485543,-0.181890537957859,
-0.590422647829571));
#15779=CARTESIAN_POINT('Ctrl Pts',(-0.816896541396381,-0.201072148666546,
-0.609616703125488));
#15780=CARTESIAN_POINT('Ctrl Pts',(-0.792310597819928,-0.223955109275652,
-0.641117951819999));
#15781=CARTESIAN_POINT('Ctrl Pts',(-0.779109323683611,-0.232742381310829,
-0.657208095763053));
#15782=CARTESIAN_POINT('Ctrl Pts',(-0.750552691816205,-0.244234834628584,
-0.68964083160521));
#15783=CARTESIAN_POINT('Ctrl Pts',(-0.735185187071673,-0.246942143572133,
-0.705971972091755));
#15784=CARTESIAN_POINT('Ctrl Pts',(-0.705971972091754,-0.246942143572133,
-0.735185187071673));
#15785=CARTESIAN_POINT('Ctrl Pts',(-0.68964083160521,-0.244234834628584,
-0.750552691816206));
#15786=CARTESIAN_POINT('Ctrl Pts',(-0.657208095763052,-0.232742381310829,
-0.779109323683612));
#15787=CARTESIAN_POINT('Ctrl Pts',(-0.641117951819998,-0.223955109275652,
-0.792310597819928));
#15788=CARTESIAN_POINT('Ctrl Pts',(-0.609616703125488,-0.201072148666545,
-0.816896541396381));
#15789=CARTESIAN_POINT('Ctrl Pts',(-0.590422647829571,-0.181890537957859,
-0.830754510485543));
#15790=CARTESIAN_POINT('Ctrl Pts',(-0.560922177770136,-0.141695629206859,
-0.850993704737257));
#15791=CARTESIAN_POINT('Ctrl Pts',(-0.54708917182331,-0.115492077056649,
-0.85981294420286));
#15792=CARTESIAN_POINT('Ctrl Pts',(-0.533674141594226,-0.0742967091364494,
-0.868149331745852));
#15793=CARTESIAN_POINT('Ctrl Pts',(-0.530395067942936,-0.0609922781173484,
-0.870146645090731));
#15794=CARTESIAN_POINT('Ctrl Pts',(-0.528110872004958,-0.0476300000000001,
-0.871530771444223));
#15795=CARTESIAN_POINT('',(-0.242834539687906,-0.04763,-0.989696097314));
#15796=CARTESIAN_POINT('Origin',(0.,-0.04763,0.));
#15797=CARTESIAN_POINT('',(0.242834539687906,-0.04763,-0.989696097314));
#15798=CARTESIAN_POINT('Ctrl Pts',(-0.242834539687907,-0.04763,-0.989696097314));
#15799=CARTESIAN_POINT('Ctrl Pts',(-0.24024064412003,-0.0609922781173483,
-0.990332542620729));
#15800=CARTESIAN_POINT('Ctrl Pts',(-0.236509675094874,-0.0742967091364493,
-0.991238884025248));
#15801=CARTESIAN_POINT('Ctrl Pts',(-0.221129100087819,-0.115492077056649,
-0.994830026707808));
#15802=CARTESIAN_POINT('Ctrl Pts',(-0.205111543747588,-0.141695629206859,
-0.998375294985966));
#15803=CARTESIAN_POINT('Ctrl Pts',(-0.169940289819232,-0.181890537957859,
-1.00492400591205));
#15804=CARTESIAN_POINT('Ctrl Pts',(-0.1465689792446,-0.201072148666545,
-1.00869718865384));
#15805=CARTESIAN_POINT('Ctrl Pts',(-0.106909345252087,-0.223955109275652,
-1.01358704779679));
#15806=CARTESIAN_POINT('Ctrl Pts',(-0.0861971848975942,-0.232742381310829,
-1.0156297872271));
#15807=CARTESIAN_POINT('Ctrl Pts',(-0.0430711894098823,-0.244234834628584,
-1.01837060663223));
#15808=CARTESIAN_POINT('Ctrl Pts',(-0.0206568624125606,-0.246942143572133,
-1.019052));
#15809=CARTESIAN_POINT('Ctrl Pts',(0.0206568624125607,-0.246942143572133,
-1.019052));
#15810=CARTESIAN_POINT('Ctrl Pts',(0.0430711894098824,-0.244234834628584,
-1.01837060663223));
#15811=CARTESIAN_POINT('Ctrl Pts',(0.0861971848975943,-0.232742381310829,
-1.0156297872271));
#15812=CARTESIAN_POINT('Ctrl Pts',(0.106909345252088,-0.223955109275652,
-1.01358704779679));
#15813=CARTESIAN_POINT('Ctrl Pts',(0.1465689792446,-0.201072148666545,-1.00869718865384));
#15814=CARTESIAN_POINT('Ctrl Pts',(0.169940289819232,-0.181890537957859,
-1.00492400591205));
#15815=CARTESIAN_POINT('Ctrl Pts',(0.205111543747588,-0.141695629206859,
-0.998375294985966));
#15816=CARTESIAN_POINT('Ctrl Pts',(0.221129100087819,-0.115492077056649,
-0.994830026707808));
#15817=CARTESIAN_POINT('Ctrl Pts',(0.236509675094874,-0.0742967091364493,
-0.991238884025248));
#15818=CARTESIAN_POINT('Ctrl Pts',(0.24024064412003,-0.0609922781173484,
-0.990332542620729));
#15819=CARTESIAN_POINT('Ctrl Pts',(0.242834539687907,-0.04763,-0.989696097314));
#15820=CARTESIAN_POINT('',(0.528110872004958,-0.04763,-0.871530771444223));
#15821=CARTESIAN_POINT('Origin',(0.,-0.04763,0.));
#15822=CARTESIAN_POINT('',(0.871530771444223,-0.04763,-0.528110872004958));
#15823=CARTESIAN_POINT('Ctrl Pts',(0.528110872004958,-0.0476300000000001,
-0.871530771444223));
#15824=CARTESIAN_POINT('Ctrl Pts',(0.530395067942936,-0.0609922781173484,
-0.870146645090731));
#15825=CARTESIAN_POINT('Ctrl Pts',(0.533674141594226,-0.0742967091364493,
-0.868149331745851));
#15826=CARTESIAN_POINT('Ctrl Pts',(0.54708917182331,-0.115492077056649,
-0.85981294420286));
#15827=CARTESIAN_POINT('Ctrl Pts',(0.560922177770136,-0.141695629206859,
-0.850993704737257));
#15828=CARTESIAN_POINT('Ctrl Pts',(0.590422647829571,-0.181890537957859,
-0.830754510485543));
#15829=CARTESIAN_POINT('Ctrl Pts',(0.609616703125488,-0.201072148666545,
-0.816896541396381));
#15830=CARTESIAN_POINT('Ctrl Pts',(0.641117951819998,-0.223955109275652,
-0.792310597819928));
#15831=CARTESIAN_POINT('Ctrl Pts',(0.657208095763053,-0.232742381310829,
-0.779109323683612));
#15832=CARTESIAN_POINT('Ctrl Pts',(0.68964083160521,-0.244234834628584,
-0.750552691816206));
#15833=CARTESIAN_POINT('Ctrl Pts',(0.705971972091755,-0.246942143572133,
-0.735185187071673));
#15834=CARTESIAN_POINT('Ctrl Pts',(0.735185187071673,-0.246942143572133,
-0.705971972091754));
#15835=CARTESIAN_POINT('Ctrl Pts',(0.750552691816206,-0.244234834628584,
-0.68964083160521));
#15836=CARTESIAN_POINT('Ctrl Pts',(0.779109323683612,-0.232742381310829,
-0.657208095763053));
#15837=CARTESIAN_POINT('Ctrl Pts',(0.792310597819928,-0.223955109275652,
-0.641117951819998));
#15838=CARTESIAN_POINT('Ctrl Pts',(0.816896541396381,-0.201072148666545,
-0.609616703125488));
#15839=CARTESIAN_POINT('Ctrl Pts',(0.830754510485543,-0.181890537957859,
-0.590422647829571));
#15840=CARTESIAN_POINT('Ctrl Pts',(0.850993704737257,-0.141695629206859,
-0.560922177770136));
#15841=CARTESIAN_POINT('Ctrl Pts',(0.85981294420286,-0.115492077056649,
-0.54708917182331));
#15842=CARTESIAN_POINT('Ctrl Pts',(0.868149331745851,-0.0742967091364493,
-0.533674141594226));
#15843=CARTESIAN_POINT('Ctrl Pts',(0.870146645090731,-0.0609922781173484,
-0.530395067942936));
#15844=CARTESIAN_POINT('Ctrl Pts',(0.871530771444223,-0.0476300000000001,
-0.528110872004958));
#15845=CARTESIAN_POINT('',(0.989696097314,-0.04763,-0.242834539687906));
#15846=CARTESIAN_POINT('Origin',(0.,-0.04763,0.));
#15847=CARTESIAN_POINT('',(0.989696097314,-0.04763,0.242834539687906));
#15848=CARTESIAN_POINT('Ctrl Pts',(0.989696097314,-0.04763,-0.242834539687907));
#15849=CARTESIAN_POINT('Ctrl Pts',(0.990332542620729,-0.0609922781173483,
-0.24024064412003));
#15850=CARTESIAN_POINT('Ctrl Pts',(0.991238884025248,-0.0742967091364493,
-0.236509675094874));
#15851=CARTESIAN_POINT('Ctrl Pts',(0.994830026707808,-0.115492077056649,
-0.221129100087819));
#15852=CARTESIAN_POINT('Ctrl Pts',(0.998375294985966,-0.141695629206859,
-0.205111543747588));
#15853=CARTESIAN_POINT('Ctrl Pts',(1.00492400591205,-0.181890537957859,
-0.169940289819232));
#15854=CARTESIAN_POINT('Ctrl Pts',(1.00869718865384,-0.201072148666545,
-0.1465689792446));
#15855=CARTESIAN_POINT('Ctrl Pts',(1.01358704779679,-0.223955109275652,
-0.106909345252087));
#15856=CARTESIAN_POINT('Ctrl Pts',(1.0156297872271,-0.232742381310829,-0.0861971848975942));
#15857=CARTESIAN_POINT('Ctrl Pts',(1.01837060663223,-0.244234834628584,
-0.0430711894098823));
#15858=CARTESIAN_POINT('Ctrl Pts',(1.019052,-0.246942143572133,-0.0206568624125607));
#15859=CARTESIAN_POINT('Ctrl Pts',(1.019052,-0.246942143572133,0.0206568624125607));
#15860=CARTESIAN_POINT('Ctrl Pts',(1.01837060663223,-0.244234834628584,
0.0430711894098823));
#15861=CARTESIAN_POINT('Ctrl Pts',(1.0156297872271,-0.232742381310829,0.0861971848975942));
#15862=CARTESIAN_POINT('Ctrl Pts',(1.01358704779679,-0.223955109275652,
0.106909345252087));
#15863=CARTESIAN_POINT('Ctrl Pts',(1.00869718865384,-0.201072148666545,
0.1465689792446));
#15864=CARTESIAN_POINT('Ctrl Pts',(1.00492400591205,-0.181890537957859,
0.169940289819232));
#15865=CARTESIAN_POINT('Ctrl Pts',(0.998375294985966,-0.141695629206859,
0.205111543747588));
#15866=CARTESIAN_POINT('Ctrl Pts',(0.994830026707808,-0.115492077056649,
0.221129100087819));
#15867=CARTESIAN_POINT('Ctrl Pts',(0.991238884025248,-0.0742967091364492,
0.236509675094874));
#15868=CARTESIAN_POINT('Ctrl Pts',(0.990332542620729,-0.0609922781173483,
0.24024064412003));
#15869=CARTESIAN_POINT('Ctrl Pts',(0.989696097314,-0.04763,0.242834539687907));
#15870=CARTESIAN_POINT('Origin',(0.,-0.04763,0.));
#15871=CARTESIAN_POINT('Origin',(0.,-0.04763,0.));
#15872=CARTESIAN_POINT('',(0.238183666596899,-0.04763,0.951592097314));
#15873=CARTESIAN_POINT('Origin',(0.,-0.04763,0.));
#15874=CARTESIAN_POINT('Origin',(-1.94289029309402E-16,-0.04763,1.));
#15875=CARTESIAN_POINT('Origin',(-1.94289029309402E-16,0.,1.));
#15876=CARTESIAN_POINT('',(-0.2381836665969,-0.04763,0.951592097314));
#15877=CARTESIAN_POINT('Ctrl Pts',(-0.238183666596899,-0.0476299999999999,
0.951592097314));
#15878=CARTESIAN_POINT('Ctrl Pts',(-0.233157223576062,-0.0740444353928835,
0.952850216871763));
#15879=CARTESIAN_POINT('Ctrl Pts',(-0.223801617934946,-0.0999305678883309,
0.955173119738174));
#15880=CARTESIAN_POINT('Ctrl Pts',(-0.199966927975188,-0.142345102874864,
0.960411259488514));
#15881=CARTESIAN_POINT('Ctrl Pts',(-0.1868781821531,-0.159766064500479,
0.963103647174702));
#15882=CARTESIAN_POINT('Ctrl Pts',(-0.15681442133453,-0.190326085855194,
0.968453058988463));
#15883=CARTESIAN_POINT('Ctrl Pts',(-0.139836317888043,-0.203463743702801,
0.971100730005489));
#15884=CARTESIAN_POINT('Ctrl Pts',(-0.104422493053067,-0.224161999508995,
0.975530745318961));
#15885=CARTESIAN_POINT('Ctrl Pts',(-0.0842175114474176,-0.232861760990032,
0.977553872336861));
#15886=CARTESIAN_POINT('Ctrl Pts',(-0.0421062857595701,-0.244251601209411,
0.980270995488453));
#15887=CARTESIAN_POINT('Ctrl Pts',(-0.0201990724523197,-0.246942143572133,
0.980948));
#15888=CARTESIAN_POINT('Ctrl Pts',(0.020199072452319,-0.246942143572133,
0.980948));
#15889=CARTESIAN_POINT('Ctrl Pts',(0.0421062857595694,-0.244251601209411,
0.980270995488454));
#15890=CARTESIAN_POINT('Ctrl Pts',(0.0842175114474169,-0.232861760990032,
0.977553872336861));
#15891=CARTESIAN_POINT('Ctrl Pts',(0.104422493053067,-0.224161999508995,
0.975530745318961));
#15892=CARTESIAN_POINT('Ctrl Pts',(0.139836317888042,-0.203463743702801,
0.971100730005489));
#15893=CARTESIAN_POINT('Ctrl Pts',(0.15681442133453,-0.190326085855194,
0.968453058988463));
#15894=CARTESIAN_POINT('Ctrl Pts',(0.1868781821531,-0.15976606450048,0.963103647174702));
#15895=CARTESIAN_POINT('Ctrl Pts',(0.199966927975188,-0.142345102874864,
0.960411259488514));
#15896=CARTESIAN_POINT('Ctrl Pts',(0.223801617934945,-0.0999305678883309,
0.955173119738174));
#15897=CARTESIAN_POINT('Ctrl Pts',(0.233157223576061,-0.0740444353928835,
0.952850216871763));
#15898=CARTESIAN_POINT('Ctrl Pts',(0.238183666596899,-0.0476299999999999,
0.951592097314));
#15899=CARTESIAN_POINT('Origin',(-1.94289029309402E-16,-0.04763,1.));
#15900=CARTESIAN_POINT('Origin',(0.,-0.04763,0.));
#15901=CARTESIAN_POINT('',(-0.504455939115715,-0.04763,0.841298510752802));
#15902=CARTESIAN_POINT('Origin',(0.,-0.04763,0.));
#15903=CARTESIAN_POINT('Origin',(-0.707106781186548,-0.04763,0.707106781186547));
#15904=CARTESIAN_POINT('Origin',(-0.707106781186548,0.,0.707106781186547));
#15905=CARTESIAN_POINT('',(-0.841298510752802,-0.04763,0.504455939115715));
#15906=CARTESIAN_POINT('Ctrl Pts',(-0.841298510752802,-0.04763,0.504455939115715));
#15907=CARTESIAN_POINT('Ctrl Pts',(-0.838633903678357,-0.0740444353928835,
0.508899795931835));
#15908=CARTESIAN_POINT('Ctrl Pts',(-0.833661031856294,-0.0999305678883309,
0.517157748491652));
#15909=CARTESIAN_POINT('Ctrl Pts',(-0.820511285096538,-0.142345102874864,
0.537715343527944));
#15910=CARTESIAN_POINT('Ctrl Pts',(-0.813159949759,-0.159766064500479,0.548874290046456));
#15911=CARTESIAN_POINT('Ctrl Pts',(-0.795684265985089,-0.190326085855194,
0.573915184558107));
#15912=CARTESIAN_POINT('Ctrl Pts',(-0.78555112003688,-0.203463743702801,
0.587792702767295));
#15913=CARTESIAN_POINT('Ctrl Pts',(-0.763642258217233,-0.224161999508995,
0.615966552324775));
#15914=CARTESIAN_POINT('Ctrl Pts',(-0.750785745543687,-0.232861760990032,
0.631684198665438));
#15915=CARTESIAN_POINT('Ctrl Pts',(-0.722929908501543,-0.244251601209411,
0.663382628119203));
#15916=CARTESIAN_POINT('Ctrl Pts',(-0.707917883896095,-0.246942143572133,
0.679352081686668));
#15917=CARTESIAN_POINT('Ctrl Pts',(-0.679352081686668,-0.246942143572133,
0.707917883896095));
#15918=CARTESIAN_POINT('Ctrl Pts',(-0.663382628119203,-0.244251601209411,
0.722929908501544));
#15919=CARTESIAN_POINT('Ctrl Pts',(-0.631684198665438,-0.232861760990031,
0.750785745543687));
#15920=CARTESIAN_POINT('Ctrl Pts',(-0.615966552324775,-0.224161999508995,
0.763642258217233));
#15921=CARTESIAN_POINT('Ctrl Pts',(-0.587792702767295,-0.203463743702801,
0.78555112003688));
#15922=CARTESIAN_POINT('Ctrl Pts',(-0.573915184558107,-0.190326085855194,
0.795684265985088));
#15923=CARTESIAN_POINT('Ctrl Pts',(-0.548874290046456,-0.159766064500479,
0.813159949759));
#15924=CARTESIAN_POINT('Ctrl Pts',(-0.537715343527944,-0.142345102874864,
0.820511285096538));
#15925=CARTESIAN_POINT('Ctrl Pts',(-0.517157748491652,-0.0999305678883309,
0.833661031856294));
#15926=CARTESIAN_POINT('Ctrl Pts',(-0.508899795931835,-0.0740444353928835,
0.838633903678357));
#15927=CARTESIAN_POINT('Ctrl Pts',(-0.504455939115716,-0.04763,0.841298510752801));
#15928=CARTESIAN_POINT('Origin',(-0.707106781186548,-0.04763,0.707106781186547));
#15929=CARTESIAN_POINT('Origin',(0.,-0.04763,0.));
#15930=CARTESIAN_POINT('',(-0.951592097314,-0.04763,0.238183666596899));
#15931=CARTESIAN_POINT('Origin',(0.,-0.04763,0.));
#15932=CARTESIAN_POINT('Origin',(-1.,-0.04763,-1.11022302462516E-16));
#15933=CARTESIAN_POINT('Origin',(-1.,0.,-1.11022302462516E-16));
#15934=CARTESIAN_POINT('',(-0.951592097314,-0.04763,-0.2381836665969));
#15935=CARTESIAN_POINT('',(-0.980948,-0.246942143572133,1.08514323328844E-18));
#15936=CARTESIAN_POINT('Ctrl Pts',(-0.951592097314,-0.04763,-0.238183666596899));
#15937=CARTESIAN_POINT('Ctrl Pts',(-0.952850216871763,-0.0740444353928835,
-0.233157223576062));
#15938=CARTESIAN_POINT('Ctrl Pts',(-0.955173119738174,-0.0999305678883309,
-0.223801617934946));
#15939=CARTESIAN_POINT('Ctrl Pts',(-0.960411259488514,-0.142345102874864,
-0.199966927975188));
#15940=CARTESIAN_POINT('Ctrl Pts',(-0.963103647174702,-0.159766064500479,
-0.1868781821531));
#15941=CARTESIAN_POINT('Ctrl Pts',(-0.968453058988463,-0.190326085855194,
-0.15681442133453));
#15942=CARTESIAN_POINT('Ctrl Pts',(-0.971100730005489,-0.203463743702801,
-0.139836317888043));
#15943=CARTESIAN_POINT('Ctrl Pts',(-0.975530745318961,-0.224161999508995,
-0.104422493053067));
#15944=CARTESIAN_POINT('Ctrl Pts',(-0.977553872336861,-0.232861760990032,
-0.0842175114474175));
#15945=CARTESIAN_POINT('Ctrl Pts',(-0.980270995488453,-0.244251601209411,
-0.0421062857595699));
#15946=CARTESIAN_POINT('Ctrl Pts',(-0.980948,-0.246942143572133,-0.0201990724523195));
#15947=CARTESIAN_POINT('Ctrl Pts',(-0.980948,-0.246942143572133,-1.17961196366423E-16));
#15948=CARTESIAN_POINT('Origin',(-1.,-0.04763,-1.11022302462516E-16));
#15949=CARTESIAN_POINT('Ctrl Pts',(-0.980948,-0.246942143572133,-1.17961196366423E-16));
#15950=CARTESIAN_POINT('Ctrl Pts',(-0.980948,-0.246942143572133,0.0201990724523192));
#15951=CARTESIAN_POINT('Ctrl Pts',(-0.980270995488453,-0.244251601209411,
0.0421062857595695));
#15952=CARTESIAN_POINT('Ctrl Pts',(-0.977553872336861,-0.232861760990032,
0.0842175114474169));
#15953=CARTESIAN_POINT('Ctrl Pts',(-0.975530745318961,-0.224161999508995,
0.104422493053066));
#15954=CARTESIAN_POINT('Ctrl Pts',(-0.971100730005489,-0.203463743702801,
0.139836317888042));
#15955=CARTESIAN_POINT('Ctrl Pts',(-0.968453058988463,-0.190326085855194,
0.15681442133453));
#15956=CARTESIAN_POINT('Ctrl Pts',(-0.963103647174702,-0.15976606450048,
0.1868781821531));
#15957=CARTESIAN_POINT('Ctrl Pts',(-0.960411259488514,-0.142345102874864,
0.199966927975188));
#15958=CARTESIAN_POINT('Ctrl Pts',(-0.955173119738174,-0.099930567888331,
0.223801617934945));
#15959=CARTESIAN_POINT('Ctrl Pts',(-0.952850216871763,-0.0740444353928835,
0.233157223576061));
#15960=CARTESIAN_POINT('Ctrl Pts',(-0.951592097314,-0.04763,0.238183666596899));
#15961=CARTESIAN_POINT('Origin',(0.,-0.04763,0.));
#15962=CARTESIAN_POINT('',(-0.841298510752802,-0.04763,-0.504455939115715));
#15963=CARTESIAN_POINT('Origin',(0.,-0.04763,0.));
#15964=CARTESIAN_POINT('Origin',(-0.707106781186547,-0.04763,-0.707106781186548));
#15965=CARTESIAN_POINT('Origin',(-0.707106781186547,0.,-0.707106781186548));
#15966=CARTESIAN_POINT('',(-0.504455939115715,-0.04763,-0.841298510752802));
#15967=CARTESIAN_POINT('Ctrl Pts',(-0.504455939115715,-0.04763,-0.841298510752802));
#15968=CARTESIAN_POINT('Ctrl Pts',(-0.508899795931835,-0.0740444353928835,
-0.838633903678357));
#15969=CARTESIAN_POINT('Ctrl Pts',(-0.517157748491652,-0.0999305678883309,
-0.833661031856294));
#15970=CARTESIAN_POINT('Ctrl Pts',(-0.537715343527944,-0.142345102874864,
-0.820511285096538));
#15971=CARTESIAN_POINT('Ctrl Pts',(-0.548874290046456,-0.159766064500479,
-0.813159949759));
#15972=CARTESIAN_POINT('Ctrl Pts',(-0.573915184558107,-0.190326085855194,
-0.795684265985089));
#15973=CARTESIAN_POINT('Ctrl Pts',(-0.587792702767295,-0.203463743702801,
-0.78555112003688));
#15974=CARTESIAN_POINT('Ctrl Pts',(-0.615966552324775,-0.224161999508995,
-0.763642258217233));
#15975=CARTESIAN_POINT('Ctrl Pts',(-0.631684198665438,-0.232861760990032,
-0.750785745543687));
#15976=CARTESIAN_POINT('Ctrl Pts',(-0.663382628119203,-0.244251601209411,
-0.722929908501543));
#15977=CARTESIAN_POINT('Ctrl Pts',(-0.679352081686668,-0.246942143572133,
-0.707917883896095));
#15978=CARTESIAN_POINT('Ctrl Pts',(-0.707917883896095,-0.246942143572133,
-0.679352081686668));
#15979=CARTESIAN_POINT('Ctrl Pts',(-0.722929908501543,-0.244251601209411,
-0.663382628119203));
#15980=CARTESIAN_POINT('Ctrl Pts',(-0.750785745543687,-0.232861760990032,
-0.631684198665439));
#15981=CARTESIAN_POINT('Ctrl Pts',(-0.763642258217232,-0.224161999508995,
-0.615966552324775));
#15982=CARTESIAN_POINT('Ctrl Pts',(-0.78555112003688,-0.203463743702801,
-0.587792702767295));
#15983=CARTESIAN_POINT('Ctrl Pts',(-0.795684265985088,-0.190326085855194,
-0.573915184558107));
#15984=CARTESIAN_POINT('Ctrl Pts',(-0.813159949759,-0.15976606450048,-0.548874290046456));
#15985=CARTESIAN_POINT('Ctrl Pts',(-0.820511285096538,-0.142345102874864,
-0.537715343527944));
#15986=CARTESIAN_POINT('Ctrl Pts',(-0.833661031856294,-0.0999305678883311,
-0.517157748491652));
#15987=CARTESIAN_POINT('Ctrl Pts',(-0.838633903678357,-0.0740444353928836,
-0.508899795931835));
#15988=CARTESIAN_POINT('Ctrl Pts',(-0.841298510752801,-0.04763,-0.504455939115715));
#15989=CARTESIAN_POINT('Origin',(-0.707106781186547,-0.04763,-0.707106781186548));
#15990=CARTESIAN_POINT('Origin',(0.,-0.04763,0.));
#15991=CARTESIAN_POINT('',(-0.238183666596899,-0.04763,-0.951592097314));
#15992=CARTESIAN_POINT('Origin',(0.,-0.04763,0.));
#15993=CARTESIAN_POINT('Origin',(5.55111512312578E-17,-0.04763,-1.));
#15994=CARTESIAN_POINT('Origin',(5.55111512312578E-17,0.,-1.));
#15995=CARTESIAN_POINT('',(0.238183666596899,-0.04763,-0.951592097314));
#15996=CARTESIAN_POINT('Ctrl Pts',(0.238183666596899,-0.04763,-0.951592097314));
#15997=CARTESIAN_POINT('Ctrl Pts',(0.233157223576062,-0.0740444353928835,
-0.952850216871763));
#15998=CARTESIAN_POINT('Ctrl Pts',(0.223801617934946,-0.099930567888331,
-0.955173119738174));
#15999=CARTESIAN_POINT('Ctrl Pts',(0.199966927975188,-0.142345102874864,
-0.960411259488514));
#16000=CARTESIAN_POINT('Ctrl Pts',(0.1868781821531,-0.15976606450048,-0.963103647174702));
#16001=CARTESIAN_POINT('Ctrl Pts',(0.15681442133453,-0.190326085855194,
-0.968453058988463));
#16002=CARTESIAN_POINT('Ctrl Pts',(0.139836317888042,-0.203463743702801,
-0.971100730005489));
#16003=CARTESIAN_POINT('Ctrl Pts',(0.104422493053067,-0.224161999508995,
-0.975530745318961));
#16004=CARTESIAN_POINT('Ctrl Pts',(0.0842175114474173,-0.232861760990032,
-0.977553872336861));
#16005=CARTESIAN_POINT('Ctrl Pts',(0.0421062857595698,-0.244251601209411,
-0.980270995488453));
#16006=CARTESIAN_POINT('Ctrl Pts',(0.0201990724523194,-0.246942143572133,
-0.980948));
#16007=CARTESIAN_POINT('Ctrl Pts',(-0.0201990724523193,-0.246942143572133,
-0.980948));
#16008=CARTESIAN_POINT('Ctrl Pts',(-0.0421062857595697,-0.244251601209411,
-0.980270995488453));
#16009=CARTESIAN_POINT('Ctrl Pts',(-0.0842175114474171,-0.232861760990032,
-0.977553872336861));
#16010=CARTESIAN_POINT('Ctrl Pts',(-0.104422493053067,-0.224161999508995,
-0.975530745318961));
#16011=CARTESIAN_POINT('Ctrl Pts',(-0.139836317888042,-0.203463743702801,
-0.971100730005489));
#16012=CARTESIAN_POINT('Ctrl Pts',(-0.15681442133453,-0.190326085855194,
-0.968453058988463));
#16013=CARTESIAN_POINT('Ctrl Pts',(-0.1868781821531,-0.15976606450048,-0.963103647174702));
#16014=CARTESIAN_POINT('Ctrl Pts',(-0.199966927975188,-0.142345102874864,
-0.960411259488514));
#16015=CARTESIAN_POINT('Ctrl Pts',(-0.223801617934945,-0.099930567888331,
-0.955173119738174));
#16016=CARTESIAN_POINT('Ctrl Pts',(-0.233157223576062,-0.0740444353928835,
-0.952850216871763));
#16017=CARTESIAN_POINT('Ctrl Pts',(-0.238183666596899,-0.0476299999999999,
-0.951592097314));
#16018=CARTESIAN_POINT('Origin',(5.55111512312578E-17,-0.04763,-1.));
#16019=CARTESIAN_POINT('Origin',(0.,-0.04763,0.));
#16020=CARTESIAN_POINT('',(0.504455939115715,-0.04763,-0.841298510752802));
#16021=CARTESIAN_POINT('Origin',(0.,-0.04763,0.));
#16022=CARTESIAN_POINT('Origin',(0.707106781186548,-0.04763,-0.707106781186547));
#16023=CARTESIAN_POINT('Origin',(0.707106781186548,0.,-0.707106781186547));
#16024=CARTESIAN_POINT('',(0.841298510752802,-0.04763,-0.504455939115715));
#16025=CARTESIAN_POINT('Ctrl Pts',(0.841298510752802,-0.04763,-0.504455939115715));
#16026=CARTESIAN_POINT('Ctrl Pts',(0.838633903678357,-0.0740444353928835,
-0.508899795931835));
#16027=CARTESIAN_POINT('Ctrl Pts',(0.833661031856294,-0.0999305678883309,
-0.517157748491652));
#16028=CARTESIAN_POINT('Ctrl Pts',(0.820511285096538,-0.142345102874864,
-0.537715343527944));
#16029=CARTESIAN_POINT('Ctrl Pts',(0.813159949759,-0.159766064500479,-0.548874290046456));
#16030=CARTESIAN_POINT('Ctrl Pts',(0.795684265985088,-0.190326085855194,
-0.573915184558107));
#16031=CARTESIAN_POINT('Ctrl Pts',(0.78555112003688,-0.203463743702801,
-0.587792702767295));
#16032=CARTESIAN_POINT('Ctrl Pts',(0.763642258217233,-0.224161999508995,
-0.615966552324775));
#16033=CARTESIAN_POINT('Ctrl Pts',(0.750785745543687,-0.232861760990032,
-0.631684198665438));
#16034=CARTESIAN_POINT('Ctrl Pts',(0.722929908501543,-0.244251601209411,
-0.663382628119203));
#16035=CARTESIAN_POINT('Ctrl Pts',(0.707917883896095,-0.246942143572133,
-0.679352081686668));
#16036=CARTESIAN_POINT('Ctrl Pts',(0.679352081686668,-0.246942143572133,
-0.707917883896095));
#16037=CARTESIAN_POINT('Ctrl Pts',(0.663382628119203,-0.244251601209411,
-0.722929908501543));
#16038=CARTESIAN_POINT('Ctrl Pts',(0.631684198665438,-0.232861760990032,
-0.750785745543687));
#16039=CARTESIAN_POINT('Ctrl Pts',(0.615966552324775,-0.224161999508995,
-0.763642258217232));
#16040=CARTESIAN_POINT('Ctrl Pts',(0.587792702767295,-0.203463743702801,
-0.78555112003688));
#16041=CARTESIAN_POINT('Ctrl Pts',(0.573915184558107,-0.190326085855194,
-0.795684265985088));
#16042=CARTESIAN_POINT('Ctrl Pts',(0.548874290046456,-0.159766064500479,
-0.813159949759));
#16043=CARTESIAN_POINT('Ctrl Pts',(0.537715343527944,-0.142345102874864,
-0.820511285096538));
#16044=CARTESIAN_POINT('Ctrl Pts',(0.517157748491652,-0.099930567888331,
-0.833661031856294));
#16045=CARTESIAN_POINT('Ctrl Pts',(0.508899795931835,-0.0740444353928835,
-0.838633903678357));
#16046=CARTESIAN_POINT('Ctrl Pts',(0.504455939115715,-0.04763,-0.841298510752801));
#16047=CARTESIAN_POINT('Origin',(0.707106781186548,-0.04763,-0.707106781186547));
#16048=CARTESIAN_POINT('Origin',(0.,-0.166705,0.));
#16049=CARTESIAN_POINT('',(-0.980948,-0.28578,1.20131482833E-16));
#16050=CARTESIAN_POINT('Origin',(0.,-0.28578,0.));
#16051=CARTESIAN_POINT('',(-0.980948,-0.166705,1.20131482833E-16));
#16052=CARTESIAN_POINT('',(0.951592097314,-0.04763,0.238183666596899));
#16053=CARTESIAN_POINT('Origin',(0.,-0.04763,0.));
#16054=CARTESIAN_POINT('',(0.951592097314,-0.04763,-0.238183666596899));
#16055=CARTESIAN_POINT('Ctrl Pts',(0.951592097314,-0.04763,0.238183666596899));
#16056=CARTESIAN_POINT('Ctrl Pts',(0.952850216871763,-0.0740444353928835,
0.233157223576062));
#16057=CARTESIAN_POINT('Ctrl Pts',(0.955173119738174,-0.099930567888331,
0.223801617934945));
#16058=CARTESIAN_POINT('Ctrl Pts',(0.960411259488514,-0.142345102874864,
0.199966927975188));
#16059=CARTESIAN_POINT('Ctrl Pts',(0.963103647174702,-0.15976606450048,
0.1868781821531));
#16060=CARTESIAN_POINT('Ctrl Pts',(0.968453058988463,-0.190326085855194,
0.15681442133453));
#16061=CARTESIAN_POINT('Ctrl Pts',(0.971100730005489,-0.203463743702801,
0.139836317888042));
#16062=CARTESIAN_POINT('Ctrl Pts',(0.975530745318961,-0.224161999508995,
0.104422493053067));
#16063=CARTESIAN_POINT('Ctrl Pts',(0.977553872336861,-0.232861760990032,
0.0842175114474172));
#16064=CARTESIAN_POINT('Ctrl Pts',(0.980270995488453,-0.244251601209411,
0.0421062857595697));
#16065=CARTESIAN_POINT('Ctrl Pts',(0.980948,-0.246942143572133,0.0201990724523194));
#16066=CARTESIAN_POINT('Ctrl Pts',(0.980948,-0.246942143572133,-0.0201990724523194));
#16067=CARTESIAN_POINT('Ctrl Pts',(0.980270995488453,-0.244251601209411,
-0.0421062857595697));
#16068=CARTESIAN_POINT('Ctrl Pts',(0.977553872336861,-0.232861760990032,
-0.0842175114474172));
#16069=CARTESIAN_POINT('Ctrl Pts',(0.975530745318961,-0.224161999508995,
-0.104422493053067));
#16070=CARTESIAN_POINT('Ctrl Pts',(0.971100730005489,-0.203463743702801,
-0.139836317888042));
#16071=CARTESIAN_POINT('Ctrl Pts',(0.968453058988463,-0.190326085855194,
-0.15681442133453));
#16072=CARTESIAN_POINT('Ctrl Pts',(0.963103647174702,-0.15976606450048,
-0.1868781821531));
#16073=CARTESIAN_POINT('Ctrl Pts',(0.960411259488514,-0.142345102874864,
-0.199966927975188));
#16074=CARTESIAN_POINT('Ctrl Pts',(0.955173119738174,-0.099930567888331,
-0.223801617934945));
#16075=CARTESIAN_POINT('Ctrl Pts',(0.952850216871763,-0.0740444353928835,
-0.233157223576062));
#16076=CARTESIAN_POINT('Ctrl Pts',(0.951592097314,-0.0476299999999999,-0.238183666596899));
#16077=CARTESIAN_POINT('Origin',(0.,-0.04763,0.));
#16078=CARTESIAN_POINT('Origin',(0.,-0.04763,0.));
#16079=CARTESIAN_POINT('Origin',(1.,-0.04763,0.));
#16080=CARTESIAN_POINT('Origin',(1.,0.,0.));
#16081=CARTESIAN_POINT('Origin',(1.,-0.04763,0.));
#16082=CARTESIAN_POINT('Origin',(0.,-0.28578,0.));
#16083=CARTESIAN_POINT('Origin',(0.,-0.04763,0.));
#16210=UNCERTAINTY_MEASURE_WITH_UNIT(LENGTH_MEASURE(0.001),#16282,
'DISTANCE_ACCURACY_VALUE',
'Maximum model space distance between geometric entities at asserted c
onnectivities');
#16212=UNCERTAINTY_MEASURE_WITH_UNIT(LENGTH_MEASURE(0.001),#16282,
'DISTANCE_ACCURACY_VALUE',
'Maximum model space distance between geometric entities at asserted c
onnectivities');
#16279=(
GEOMETRIC_REPRESENTATION_CONTEXT(3)
GLOBAL_UNCERTAINTY_ASSIGNED_CONTEXT((#16210))
GLOBAL_UNIT_ASSIGNED_CONTEXT((#16282,#16284,#16285))
REPRESENTATION_CONTEXT('','3D')
);
#16281=(
GEOMETRIC_REPRESENTATION_CONTEXT(3)
GLOBAL_UNCERTAINTY_ASSIGNED_CONTEXT((#16212))
GLOBAL_UNIT_ASSIGNED_CONTEXT((#16282,#16284,#16285))
REPRESENTATION_CONTEXT('','3D')
);
#16282=(
LENGTH_UNIT()
NAMED_UNIT(*)
SI_UNIT(.CENTI.,.METRE.)
);
#16284=(
NAMED_UNIT(*)
PLANE_ANGLE_UNIT()
SI_UNIT($,.RADIAN.)
);
#16285=(
NAMED_UNIT(*)
SI_UNIT($,.STERADIAN.)
SOLID_ANGLE_UNIT()
);
#16352=SHAPE_DEFINITION_REPRESENTATION(#16486,#16585);
#16486=PRODUCT_DEFINITION_SHAPE('',$,#16654);
#16585=SHAPE_REPRESENTATION('',(#10098),#16279);
#16587=PRODUCT_DEFINITION_CONTEXT('part definition',#16793,'design');
#16654=PRODUCT_DEFINITION('Cage (1)','Cage (1)',#16722,#16587);
#16722=PRODUCT_DEFINITION_FORMATION('',$,#16861);
#16793=APPLICATION_CONTEXT(
'Core Data for Automotive Mechanical Design Process');
#16794=PRODUCT_CONTEXT('part definition',#16793,'mechanical');
#16861=PRODUCT('Cage (1)','Cage (1)','Cage (1)',(#16794));
#16926=COLOUR_RGB('Grey',0.48,0.52,0.57);
#16927=FILL_AREA_STYLE_COLOUR('',#16926);
#16928=FILL_AREA_STYLE('',(#16927));
#16929=SURFACE_STYLE_FILL_AREA(#16928);
#16930=SURFACE_SIDE_STYLE('',(#16929));
#16931=SURFACE_STYLE_USAGE(.BOTH.,#16930);
#16932=PRESENTATION_STYLE_ASSIGNMENT((#16931));
ENDSEC;
END-ISO-10303-21;
